ISO-10303-21;
HEADER;
FILE_DESCRIPTION (('STEP AP214'),
    '1' );
FILE_NAME ('Part14.step',
    '2026-11-01T06:29:40',
    ( '' ),
    ( '' ),
    'SwSTEP 2.0',
    'SolidWorks 2024',
    '' );
FILE_SCHEMA (( 'AUTOMOTIVE_DESIGN' ));
ENDSEC;

DATA;
#5=SURFACE_STYLE_USAGE ( .BOTH. , #14117 ) ;
#35=ADVANCED_FACE ( 'NONE', ( #14430 ), #12479, .F. ) ;
#42=AXIS2_PLACEMENT_3D ( 'NONE', #8950, #992, #1291 ) ;
#51=LINE ( 'NONE', #155, #16644 ) ;
#71=STYLED_ITEM ( 'NONE', ( #20272 ), #8119 ) ;
#75=SURFACE_STYLE_FILL_AREA ( #19257 ) ;
#102=FACE_OUTER_BOUND ( 'NONE', #1105, .T. ) ;
#151=SURFACE_STYLE_USAGE ( .BOTH. , #18792 ) ;
#155=CARTESIAN_POINT ( 'NONE',  ( 111.4893729001366012, 129.7247684487574588, 370.0000000000000000 ) ) ;
#189=CIRCLE ( 'NONE', #15696, 2.000000000000001776 ) ;
#193=CARTESIAN_POINT ( 'NONE',  ( 53.48937290013657986, 209.1356689931817243, 347.4957642363283412 ) ) ;
#207=CARTESIAN_POINT ( 'NONE',  ( 55.98937290013660828, 143.5567736071463401, 294.7336993003747239 ) ) ;
#209=( NAMED_UNIT ( * ) PLANE_ANGLE_UNIT ( ) SI_UNIT ( $, .RADIAN. ) );
#214=ORIENTED_EDGE ( 'NONE', *, *, #11946, .T. ) ;
#223=EDGE_LOOP ( 'NONE', ( #20266, #17142, #2719, #16147, #10756, #6546, #7481, #19067, #9107, #14805, #17273, #15955 ) ) ;
#232=SURFACE_STYLE_FILL_AREA ( #12504 ) ;
#258=VERTEX_POINT ( 'NONE', #7740 ) ;
#259=( NAMED_UNIT ( * ) PLANE_ANGLE_UNIT ( ) SI_UNIT ( $, .RADIAN. ) );
#274=CARTESIAN_POINT ( 'NONE',  ( -77.99033078109007988, 125.7247684487574304, 252.0000000000000000 ) ) ;
#275=( NAMED_UNIT ( * ) PLANE_ANGLE_UNIT ( ) SI_UNIT ( $, .RADIAN. ) );
#279=DIRECTION ( 'NONE',  ( 9.815121534730717399E-17, -1.000000000000000000, 0.000000000000000000 ) ) ;
#292=UNCERTAINTY_MEASURE_WITH_UNIT (LENGTH_MEASURE( 1.000000000000000082E-05 ), #17456, 'distance_accuracy_value', 'NONE');
#323=VERTEX_POINT ( 'NONE', #2782 ) ;
#338=VECTOR ( 'NONE', #7157, 1000.000000000000227 ) ;
#352=SURFACE_STYLE_USAGE ( .BOTH. , #14777 ) ;
#360=( NAMED_UNIT ( * ) PLANE_ANGLE_UNIT ( ) SI_UNIT ( $, .RADIAN. ) );
#405=CARTESIAN_POINT ( 'NONE',  ( 55.48937290013660117, 129.7247684487574588, 370.0000000000000000 ) ) ;
#407=EDGE_CURVE ( 'NONE', #6644, #18079, #6406, .T. ) ;
#429=LINE ( 'NONE', #627, #7057 ) ;
#442=EDGE_LOOP ( 'NONE', ( #17497, #7680, #6734, #2124 ) ) ;
#465=CARTESIAN_POINT ( 'NONE',  ( 111.4893729001366012, 127.7247684487574588, 370.0000000000000000 ) ) ;
#466=DIRECTION ( 'NONE',  ( 1.000000000000000000, 9.815121534730718631E-17, 0.000000000000000000 ) ) ;
#491=VECTOR ( 'NONE', #5469, 1000.000000000000000 ) ;
#501=COLOUR_RGB ( '', 0.72549020, 0.75294118, 0.79215686) ;
#521=( NAMED_UNIT ( * ) SI_UNIT ( $, .STERADIAN. ) SOLID_ANGLE_UNIT ( ) );
#538=ADVANCED_FACE ( 'NONE', ( #5357, #3709 ), #13302, .T. ) ;
#573=ORIENTED_EDGE ( 'NONE', *, *, #710, .T. ) ;
#610=PLANE ( 'NONE',  #16307 ) ;
#624=VECTOR ( 'NONE', #19346, 1000.000000000000000 ) ;
#626=CARTESIAN_POINT ( 'NONE',  ( 55.98937290013660117, 144.5787140289007198, 293.4524157190248275 ) ) ;
#627=CARTESIAN_POINT ( 'NONE',  ( 111.4893729001366154, 77.72476844875745883, 250.0000000000000000 ) ) ;
#638=CARTESIAN_POINT ( 'NONE',  ( 111.4893729001366012, 127.7247684487574588, 368.0000000000000000 ) ) ;
#639=COLOUR_RGB ( '', 0.66274510, 0.83137255, 0.94901961) ;
#651=CARTESIAN_POINT ( 'NONE',  ( 111.4893729001366154, 49.66333933884488516, 252.0000000000000000 ) ) ;
#668=VECTOR ( 'NONE', #2486, 1000.000000000000114 ) ;
#670=ORIENTED_EDGE ( 'NONE', *, *, #7353, .F. ) ;
#671=DIRECTION ( 'NONE',  ( 1.000000000000000000, 9.815121534730717399E-17, 0.000000000000000000 ) ) ;
#693=VERTEX_POINT ( 'NONE', #1085 ) ;
#710=EDGE_CURVE ( 'NONE', #1294, #4484, #4521, .T. ) ;
#725=MECHANICAL_DESIGN_GEOMETRIC_PRESENTATION_REPRESENTATION('',(#15898),#10286);
#749=UNCERTAINTY_MEASURE_WITH_UNIT (LENGTH_MEASURE( 1.000000000000000082E-05 ), #9296, 'distance_accuracy_value', 'NONE');
#752=ORIENTED_EDGE ( 'NONE', *, *, #1611, .F. ) ;
#753=FACE_OUTER_BOUND ( 'NONE', #19102, .T. ) ;
#754=CARTESIAN_POINT ( 'NONE',  ( 55.48937290013660117, 127.7247684487574588, 370.0000000000000000 ) ) ;
#768=ORIENTED_EDGE ( 'NONE', *, *, #15496, .T. ) ;
#776=SURFACE_STYLE_FILL_AREA ( #13478 ) ;
#777=LINE ( 'NONE', #17700, #16236 ) ;
#782=( GEOMETRIC_REPRESENTATION_CONTEXT ( 3 ) GLOBAL_UNCERTAINTY_ASSIGNED_CONTEXT ( ( #5189 ) ) GLOBAL_UNIT_ASSIGNED_CONTEXT ( ( #19529, #3895, #15120 ) ) REPRESENTATION_CONTEXT ( 'NONE', 'WORKASPACE' ) );
#790=LINE ( 'NONE', #6908, #624 ) ;
#802=FILL_AREA_STYLE_COLOUR ( '', #12303 ) ;
#808=ADVANCED_FACE ( 'NONE', ( #15862 ), #15983, .T. ) ;
#811=SURFACE_STYLE_USAGE ( .BOTH. , #14948 ) ;
#818=PRESENTATION_STYLE_ASSIGNMENT (( #9905 ) ) ;
#882=DIRECTION ( 'NONE',  ( -9.815121534730717399E-17, 1.000000000000000000, -2.352167425053297897E-16 ) ) ;
#885=CARTESIAN_POINT ( 'NONE',  ( 53.48937290013659407, 129.7247684487574304, 252.0000000000000000 ) ) ;
#889=VERTEX_POINT ( 'NONE', #8327 ) ;
#893=FILL_AREA_STYLE ('',( #20161 ) ) ;
#899=( NAMED_UNIT ( * ) PLANE_ANGLE_UNIT ( ) SI_UNIT ( $, .RADIAN. ) );
#901=DIRECTION ( 'NONE',  ( 1.000000000000000000, 0.000000000000000000, 0.000000000000000000 ) ) ;
#960=MECHANICAL_DESIGN_GEOMETRIC_PRESENTATION_REPRESENTATION('',(#5921),#18084);
#988=PRESENTATION_STYLE_ASSIGNMENT (( #7313 ) ) ;
#992=DIRECTION ( 'NONE',  ( 1.000000000000000000, 9.815121534730717399E-17, -0.000000000000000000 ) ) ;
#1007=SURFACE_STYLE_USAGE ( .BOTH. , #19861 ) ;
#1017=CARTESIAN_POINT ( 'NONE',  ( 111.4893729001366012, 125.7247684487574588, 254.0000000000000000 ) ) ;
#1035=LINE ( 'NONE', #16950, #8368 ) ;
#1039=ORIENTED_EDGE ( 'NONE', *, *, #16196, .F. ) ;
#1047=COLOUR_RGB ( '', 0.72549020, 0.75294118, 0.79215686) ;
#1063=CLOSED_SHELL ( 'NONE', ( #8010, #12465, #4658, #16452, #19670, #16014, #5113, #14788, #8119, #16397 ) ) ;
#1085=CARTESIAN_POINT ( 'NONE',  ( 111.4893729001366012, 127.7247684487574588, 254.0000000000000000 ) ) ;
#1091=LINE ( 'NONE', #4225, #11403 ) ;
#1098=EDGE_CURVE ( 'NONE', #5632, #693, #1571, .T. ) ;
#1104=VECTOR ( 'NONE', #4019, 1000.000000000000000 ) ;
#1105=EDGE_LOOP ( 'NONE', ( #11410, #14369, #14768, #14708 ) ) ;
#1126=SURFACE_STYLE_FILL_AREA ( #18353 ) ;
#1141=DIRECTION ( 'NONE',  ( 9.815121534730717399E-17, -1.000000000000000000, 0.000000000000000000 ) ) ;
#1164=CARTESIAN_POINT ( 'NONE',  ( 108.9893729001366012, 144.5787140289007766, 293.4524157190247138 ) ) ;
#1165=CARTESIAN_POINT ( 'NONE',  ( 111.4893729001366012, 127.7247684487574588, 254.0000000000000000 ) ) ;
#1167=FILL_AREA_STYLE_COLOUR ( '', #3110 ) ;
#1173=DIRECTION ( 'NONE',  ( 0.000000000000000000, 2.352167425053297897E-16, 1.000000000000000000 ) ) ;
#1179=ORIENTED_EDGE ( 'NONE', *, *, #5983, .T. ) ;
#1186=CARTESIAN_POINT ( 'NONE',  ( 109.4893729001366012, 129.7247684487574588, 370.0000000000000000 ) ) ;
#1191=PLANE ( 'NONE',  #16362 ) ;
#1197=PRESENTATION_STYLE_ASSIGNMENT (( #11962 ) ) ;
#1226=DIRECTION ( 'NONE',  ( 0.000000000000000000, 0.000000000000000000, 1.000000000000000000 ) ) ;
#1244=VECTOR ( 'NONE', #5317, 1000.000000000000000 ) ;
#1291=DIRECTION ( 'NONE',  ( -9.815121534730717399E-17, 1.000000000000000000, 0.000000000000000000 ) ) ;
#1294=VERTEX_POINT ( 'NONE', #2808 ) ;
#1337=CARTESIAN_POINT ( 'NONE',  ( 53.48937290013658696, 126.1646452518344859, 322.0399576098686225 ) ) ;
#1343=EDGE_LOOP ( 'NONE', ( #7833, #10893, #10967, #8608 ) ) ;
#1372=( GEOMETRIC_REPRESENTATION_CONTEXT ( 3 ) GLOBAL_UNCERTAINTY_ASSIGNED_CONTEXT ( ( #15779 ) ) GLOBAL_UNIT_ASSIGNED_CONTEXT ( ( #7156, #9093, #4162 ) ) REPRESENTATION_CONTEXT ( 'NONE', 'WORKASPACE' ) );
#1376=VERTEX_POINT ( 'NONE', #17236 ) ;
#1385=( NAMED_UNIT ( * ) PLANE_ANGLE_UNIT ( ) SI_UNIT ( $, .RADIAN. ) );
#1387=CLOSED_SHELL ( 'NONE', ( #13518, #808, #12135, #8402, #2091, #17761, #6762, #1836, #15290, #17155, #8765, #538, #17542, #10774, #12423, #12075, #3760, #35, #6916, #3060, #10404, #11440 ) ) ;
#1393=DIRECTION ( 'NONE',  ( 1.000000000000000000, 9.815121534730717399E-17, 0.000000000000000000 ) ) ;
#1395=EDGE_CURVE ( 'NONE', #7933, #10796, #14953, .T. ) ;
#1417=COLOUR_RGB ( '', 0.09019608, 0.27058824, 0.51372549) ;
#1448=STYLED_ITEM ( 'NONE', ( #18775 ), #19670 ) ;
#1459=SURFACE_SIDE_STYLE ('',( #232 ) ) ;
#1476=EDGE_CURVE ( 'NONE', #19519, #15351, #429, .T. ) ;
#1481=( NAMED_UNIT ( * ) PLANE_ANGLE_UNIT ( ) SI_UNIT ( $, .RADIAN. ) );
#1483=FILL_AREA_STYLE_COLOUR ( '', #11803 ) ;
#1491=SURFACE_SIDE_STYLE ('',( #14182 ) ) ;
#1502=( LENGTH_UNIT ( ) NAMED_UNIT ( * ) SI_UNIT ( .MILLI., .METRE. ) );
#1504=( LENGTH_UNIT ( ) NAMED_UNIT ( * ) SI_UNIT ( .MILLI., .METRE. ) );
#1526=SURFACE_STYLE_FILL_AREA ( #9391 ) ;
#1542=ORIENTED_EDGE ( 'NONE', *, *, #14940, .T. ) ;
#1543=FILL_AREA_STYLE ('',( #11059 ) ) ;
#1552=( NAMED_UNIT ( * ) SI_UNIT ( $, .STERADIAN. ) SOLID_ANGLE_UNIT ( ) );
#1571=LINE ( 'NONE', #12431, #5122 ) ;
#1572=( NAMED_UNIT ( * ) PLANE_ANGLE_UNIT ( ) SI_UNIT ( $, .RADIAN. ) );
#1579=PRESENTATION_STYLE_ASSIGNMENT (( #19229 ) ) ;
#1611=EDGE_CURVE ( 'NONE', #16025, #5632, #4037, .T. ) ;
#1616=ORIENTED_EDGE ( 'NONE', *, *, #11550, .T. ) ;
#1621=CARTESIAN_POINT ( 'NONE',  ( 108.9893729001365870, 143.5567736071463969, 294.7336993003747239 ) ) ;
#1623=( NAMED_UNIT ( * ) SI_UNIT ( $, .STERADIAN. ) SOLID_ANGLE_UNIT ( ) );
#1641=DIRECTION ( 'NONE',  ( 1.000000000000000000, 9.815121534730718631E-17, -0.000000000000000000 ) ) ;
#1672=EDGE_CURVE ( 'NONE', #16358, #9405, #3784, .T. ) ;
#1698=MECHANICAL_DESIGN_GEOMETRIC_PRESENTATION_REPRESENTATION('',(#19469),#15570);
#1702=PRESENTATION_STYLE_ASSIGNMENT (( #4831 ) ) ;
#1716=CARTESIAN_POINT ( 'NONE',  ( 53.48937290013659407, 208.2227610943810134, 346.7612763259490407 ) ) ;
#1736=PRESENTATION_STYLE_ASSIGNMENT (( #5 ) ) ;
#1743=ORIENTED_EDGE ( 'NONE', *, *, #2449, .F. ) ;
#1753=FACE_OUTER_BOUND ( 'NONE', #8175, .T. ) ;
#1777=COLOUR_RGB ( '', 0.31764706, 0.68627451, 0.89019608) ;
#1805=COLOUR_RGB ( '', 0.08235294, 0.09019608, 0.10196078) ;
#1813=AXIS2_PLACEMENT_3D ( 'NONE', #18675, #1226, #9194 ) ;
#1822=DIRECTION ( 'NONE',  ( 1.000000000000000000, 9.815121534730718631E-17, -0.000000000000000000 ) ) ;
#1835=SURFACE_STYLE_FILL_AREA ( #11215 ) ;
#1836=ADVANCED_FACE ( 'NONE', ( #17832 ), #1857, .T. ) ;
#1850=SURFACE_STYLE_USAGE ( .BOTH. , #16209 ) ;
#1857=CYLINDRICAL_SURFACE ( 'NONE', #18262, 2.000000000000001776 ) ;
#1893=FACE_OUTER_BOUND ( 'NONE', #11740, .T. ) ;
#1926=VECTOR ( 'NONE', #8747, 1000.000000000000000 ) ;
#1952=( GEOMETRIC_REPRESENTATION_CONTEXT ( 3 ) GLOBAL_UNCERTAINTY_ASSIGNED_CONTEXT ( ( #14651 ) ) GLOBAL_UNIT_ASSIGNED_CONTEXT ( ( #15966, #11096, #13991 ) ) REPRESENTATION_CONTEXT ( 'NONE', 'WORKASPACE' ) );
#1961=PRESENTATION_STYLE_ASSIGNMENT (( #3540 ) ) ;
#2010=AXIS2_PLACEMENT_3D ( 'NONE', #17468, #14181, #4705 ) ;
#2012=( LENGTH_UNIT ( ) NAMED_UNIT ( * ) SI_UNIT ( .MILLI., .METRE. ) );
#2023=VECTOR ( 'NONE', #12615, 1000.000000000000000 ) ;
#2082=EDGE_CURVE ( 'NONE', #3644, #6446, #11711, .T. ) ;
#2091=ADVANCED_FACE ( 'NONE', ( #753 ), #12408, .T. ) ;
#2092=CARTESIAN_POINT ( 'NONE',  ( 108.9893729001365870, 143.7407018517681649, 294.8816803532602080 ) ) ;
#2124=ORIENTED_EDGE ( 'NONE', *, *, #3129, .T. ) ;
#2142=ORIENTED_EDGE ( 'NONE', *, *, #7255, .F. ) ;
#2146=ORIENTED_EDGE ( 'NONE', *, *, #19640, .T. ) ;
#2152=CARTESIAN_POINT ( 'NONE',  ( 110.6609457753903882, 211.0574367717017594, 346.4752554294134939 ) ) ;
#2161=VERTEX_POINT ( 'NONE', #18575 ) ;
#2162=( LENGTH_UNIT ( ) NAMED_UNIT ( * ) SI_UNIT ( .MILLI., .METRE. ) );
#2177=CARTESIAN_POINT ( 'NONE',  ( 53.48937290013659407, 127.7247684487574304, 252.0000000000000000 ) ) ;
#2178=PRESENTATION_STYLE_ASSIGNMENT (( #10029 ) ) ;
#2206=SURFACE_STYLE_FILL_AREA ( #17881 ) ;
#2219=FILL_AREA_STYLE_COLOUR ( '', #9882 ) ;
#2257=UNCERTAINTY_MEASURE_WITH_UNIT (LENGTH_MEASURE( 1.000000000000000082E-05 ), #17186, 'distance_accuracy_value', 'NONE');
#2262=DIRECTION ( 'NONE',  ( -9.815121534730717399E-17, 1.000000000000000000, 0.000000000000000000 ) ) ;
#2286=UNCERTAINTY_MEASURE_WITH_UNIT (LENGTH_MEASURE( 1.000000000000000082E-05 ), #1502, 'distance_accuracy_value', 'NONE');
#2294=VECTOR ( 'NONE', #19645, 1000.000000000000000 ) ;
#2299=CARTESIAN_POINT ( 'NONE',  ( 53.48937290013659407, 211.0574367717017594, 346.4752554294135507 ) ) ;
#2326=DIRECTION ( 'NONE',  ( 2.125007447556912624E-15, -0.7817866094812263578, -0.6235460666509320404 ) ) ;
#2337=ORIENTED_EDGE ( 'NONE', *, *, #17605, .F. ) ;
#2351=EDGE_CURVE ( 'NONE', #17151, #7933, #10023, .T. ) ;
#2358=CARTESIAN_POINT ( 'NONE',  ( -77.99033078109007988, 127.7247684487574304, 357.7985149490353933 ) ) ;
#2371=VECTOR ( 'NONE', #18001, 1000.000000000000000 ) ;
#2392=STYLED_ITEM ( 'NONE', ( #1736 ), #35 ) ;
#2396=ORIENTED_EDGE ( 'NONE', *, *, #17549, .F. ) ;
#2417=VERTEX_POINT ( 'NONE', #626 ) ;
#2423=CARTESIAN_POINT ( 'NONE',  ( 53.48937290013659407, 127.7247684487574304, 252.0000000000000000 ) ) ;
#2430=LINE ( 'NONE', #16385, #13815 ) ;
#2443=FILL_AREA_STYLE_COLOUR ( '', #15541 ) ;
#2445=ORIENTED_EDGE ( 'NONE', *, *, #18313, .F. ) ;
#2449=EDGE_CURVE ( 'NONE', #4636, #4060, #3843, .T. ) ;
#2458=CARTESIAN_POINT ( 'NONE',  ( 53.48937290013659407, 129.7247684487574588, 283.6050404526570219 ) ) ;
#2462=PRESENTATION_STYLE_ASSIGNMENT (( #11950 ) ) ;
#2466=CARTESIAN_POINT ( 'NONE',  ( 55.98937290013660828, 108.8727366810871899, 338.2196854716659118 ) ) ;
#2480=VECTOR ( 'NONE', #14886, 1000.000000000000114 ) ;
#2486=DIRECTION ( 'NONE',  ( -0.000000000000000000, -0.7791332379872890623, -0.6268583551835633649 ) ) ;
#2508=CARTESIAN_POINT ( 'NONE',  ( 53.48937290013659407, 125.7247684487574588, 254.0000000000000000 ) ) ;
#2520=CARTESIAN_POINT ( 'NONE',  ( 53.48937290013658696, 122.8810204491430369, 322.0399576098686225 ) ) ;
#2524=EDGE_LOOP ( 'NONE', ( #16665, #9113, #6092, #1616 ) ) ;
#2537=PRESENTATION_STYLE_ASSIGNMENT (( #18091 ) ) ;
#2539=CARTESIAN_POINT ( 'NONE',  ( 53.48937290013658696, 126.1646452518344859, 280.0825295754780768 ) ) ;
#2541=PLANE ( 'NONE',  #4033 ) ;
#2544=EDGE_LOOP ( 'NONE', ( #8427, #9791 ) ) ;
#2565=CARTESIAN_POINT ( 'NONE',  ( 55.48937290013660117, 127.7247684487574588, 370.0000000000000000 ) ) ;
#2567=VERTEX_POINT ( 'NONE', #207 ) ;
#2568=ORIENTED_EDGE ( 'NONE', *, *, #18752, .F. ) ;
#2573=VERTEX_POINT ( 'NONE', #1621 ) ;
#2597=AXIS2_PLACEMENT_3D ( 'NONE', #1017, #16646, #19785 ) ;
#2636=SURFACE_STYLE_FILL_AREA ( #13481 ) ;
#2647=AXIS2_PLACEMENT_3D ( 'NONE', #10573, #4386, #15424 ) ;
#2668=CARTESIAN_POINT ( 'NONE',  ( 109.4893729001366012, 127.7247684487574588, 370.0000000000000000 ) ) ;
#2699=UNCERTAINTY_MEASURE_WITH_UNIT (LENGTH_MEASURE( 1.000000000000000082E-05 ), #8225, 'distance_accuracy_value', 'NONE');
#2716=VECTOR ( 'NONE', #14585, 1000.000000000000114 ) ;
#2719=ORIENTED_EDGE ( 'NONE', *, *, #7049, .T. ) ;
#2741=AXIS2_PLACEMENT_3D ( 'NONE', #5042, #3500, #8234 ) ;
#2781=( GEOMETRIC_REPRESENTATION_CONTEXT ( 3 ) GLOBAL_UNCERTAINTY_ASSIGNED_CONTEXT ( ( #17743 ) ) GLOBAL_UNIT_ASSIGNED_CONTEXT ( ( #2162, #3629, #5077 ) ) REPRESENTATION_CONTEXT ( 'NONE', 'WORKASPACE' ) );
#2782=CARTESIAN_POINT ( 'NONE',  ( 53.48937290013659407, 208.2227610943810134, 346.7612763259490407 ) ) ;
#2807=ORIENTED_EDGE ( 'NONE', *, *, #5374, .F. ) ;
#2808=CARTESIAN_POINT ( 'NONE',  ( 53.48937290013659407, 125.7247684487574588, 252.0000000000000000 ) ) ;
#2812=EDGE_CURVE ( 'NONE', #18079, #12831, #9056, .T. ) ;
#2825=EDGE_LOOP ( 'NONE', ( #8917, #15650, #1743, #15687 ) ) ;
#2836=( NAMED_UNIT ( * ) PLANE_ANGLE_UNIT ( ) SI_UNIT ( $, .RADIAN. ) );
#2839=CARTESIAN_POINT ( 'NONE',  ( -77.99033078109007988, 127.7247684487574304, 357.7985149490353933 ) ) ;
#2850=EDGE_LOOP ( 'NONE', ( #16383, #16030, #12262, #12254 ) ) ;
#2898=( NAMED_UNIT ( * ) SI_UNIT ( $, .STERADIAN. ) SOLID_ANGLE_UNIT ( ) );
#2901=VERTEX_POINT ( 'NONE', #5964 ) ;
#2904=LINE ( 'NONE', #13949, #15283 ) ;
#2905=( LENGTH_UNIT ( ) NAMED_UNIT ( * ) SI_UNIT ( .MILLI., .METRE. ) );
#2921=EDGE_CURVE ( 'NONE', #693, #19038, #1091, .T. ) ;
#2936=CIRCLE ( 'NONE', #13494, 3.283624802691453848 ) ;
#2945=CYLINDRICAL_SURFACE ( 'NONE', #2948, 2.000000000000001776 ) ;
#2948=AXIS2_PLACEMENT_3D ( 'NONE', #8214, #466, #11500 ) ;
#2957=DIRECTION ( 'NONE',  ( 0.000000000000000000, 1.000000000000000000, 0.000000000000000000 ) ) ;
#3000=FILL_AREA_STYLE_COLOUR ( '', #8087 ) ;
#3031=SURFACE_STYLE_USAGE ( .BOTH. , #15644 ) ;
#3036=( GEOMETRIC_REPRESENTATION_CONTEXT ( 3 ) GLOBAL_UNCERTAINTY_ASSIGNED_CONTEXT ( ( #12890 ) ) GLOBAL_UNIT_ASSIGNED_CONTEXT ( ( #19405, #10145, #14380 ) ) REPRESENTATION_CONTEXT ( 'NONE', 'WORKASPACE' ) );
#3057=FILL_AREA_STYLE_COLOUR ( '', #7409 ) ;
#3058=SURFACE_STYLE_USAGE ( .BOTH. , #14003 ) ;
#3060=ADVANCED_FACE ( 'NONE', ( #14304 ), #17295, .T. ) ;
#3064=SURFACE_STYLE_USAGE ( .BOTH. , #12772 ) ;
#3081=ORIENTED_EDGE ( 'NONE', *, *, #18666, .T. ) ;
#3085=ORIENTED_EDGE ( 'NONE', *, *, #3129, .F. ) ;
#3100=AXIS2_PLACEMENT_3D ( 'NONE', #13943, #3126, #15721 ) ;
#3106=LINE ( 'NONE', #17112, #17206 ) ;
#3110=COLOUR_RGB ( '', 0.08235294, 0.09019608, 0.10196078) ;
#3126=DIRECTION ( 'NONE',  ( -9.815121534730717399E-17, 1.000000000000000000, -2.352167425053297897E-16 ) ) ;
#3129=EDGE_CURVE ( 'NONE', #6137, #6221, #8958, .T. ) ;
#3143=EDGE_LOOP ( 'NONE', ( #9080, #12138, #14871, #7231 ) ) ;
#3173=EDGE_CURVE ( 'NONE', #18128, #14376, #777, .T. ) ;
#3177=( NAMED_UNIT ( * ) PLANE_ANGLE_UNIT ( ) SI_UNIT ( $, .RADIAN. ) );
#3180=SURFACE_STYLE_FILL_AREA ( #6481 ) ;
#3186=CARTESIAN_POINT ( 'NONE',  ( 111.4893729001366012, 122.8810204491430369, 280.0825295754780768 ) ) ;
#3220=DIRECTION ( 'NONE',  ( 0.000000000000000000, 0.7699350945217658948, 0.6381222063396316813 ) ) ;
#3232=CARTESIAN_POINT ( 'NONE',  ( 53.48937290013659407, 209.4935875941501422, 345.2279431939882670 ) ) ;
#3237=DIRECTION ( 'NONE',  ( 1.000000000000000000, 0.000000000000000000, 0.000000000000000000 ) ) ;
#3261=( GEOMETRIC_REPRESENTATION_CONTEXT ( 3 ) GLOBAL_UNCERTAINTY_ASSIGNED_CONTEXT ( ( #17765 ) ) GLOBAL_UNIT_ASSIGNED_CONTEXT ( ( #10329, #15077, #18452 ) ) REPRESENTATION_CONTEXT ( 'NONE', 'WORKASPACE' ) );
#3264=( NAMED_UNIT ( * ) PLANE_ANGLE_UNIT ( ) SI_UNIT ( $, .RADIAN. ) );
#3274=COLOUR_RGB ( '', 0.09019608, 0.27058824, 0.51372549) ;
#3283=DIRECTION ( 'NONE',  ( 0.000000000000000000, 1.000000000000000000, 0.000000000000000000 ) ) ;
#3304=( NAMED_UNIT ( * ) PLANE_ANGLE_UNIT ( ) SI_UNIT ( $, .RADIAN. ) );
#3307=VERTEX_POINT ( 'NONE', #1164 ) ;
#3314=DIRECTION ( 'NONE',  ( 0.000000000000000000, -2.352167425053297897E-16, -1.000000000000000000 ) ) ;
#3327=PLANE ( 'NONE',  #11346 ) ;
#3336=EDGE_LOOP ( 'NONE', ( #15468, #4072, #768, #5036, #18806, #214 ) ) ;
#3339=ORIENTED_EDGE ( 'NONE', *, *, #12413, .T. ) ;
#3376=DIRECTION ( 'NONE',  ( 0.000000000000000000, -0.000000000000000000, 1.000000000000000000 ) ) ;
#3377=CARTESIAN_POINT ( 'NONE',  ( 53.48937290013658696, 122.8810204491430369, 280.0825295754780768 ) ) ;
#3383=CARTESIAN_POINT ( 'NONE',  ( 53.48937290013659407, 211.0574367717017594, 346.4752554294135507 ) ) ;
#3387=MECHANICAL_DESIGN_GEOMETRIC_PRESENTATION_REPRESENTATION('',(#8647),#1372);
#3423=PRESENTATION_STYLE_ASSIGNMENT (( #19286 ) ) ;
#3427=MECHANICAL_DESIGN_GEOMETRIC_PRESENTATION_REPRESENTATION('',(#4095),#11320);
#3431=ORIENTED_EDGE ( 'NONE', *, *, #19425, .F. ) ;
#3450=AXIS2_PLACEMENT_3D ( 'NONE', #6219, #12715, #3220 ) ;
#3472=CARTESIAN_POINT ( 'NONE',  ( 108.9893729001366296, 130.3113892758443910, 284.0770112900635240 ) ) ;
#3480=( LENGTH_UNIT ( ) NAMED_UNIT ( * ) SI_UNIT ( .MILLI., .METRE. ) );
#3500=DIRECTION ( 'NONE',  ( 0.000000000000000000, 0.000000000000000000, 1.000000000000000000 ) ) ;
#3522=( LENGTH_UNIT ( ) NAMED_UNIT ( * ) SI_UNIT ( .MILLI., .METRE. ) );
#3533=LINE ( 'NONE', #14441, #7284 ) ;
#3537=UNCERTAINTY_MEASURE_WITH_UNIT (LENGTH_MEASURE( 1.000000000000000082E-05 ), #6314, 'distance_accuracy_value', 'NONE');
#3540=SURFACE_STYLE_USAGE ( .BOTH. , #17653 ) ;
#3592=PRESENTATION_STYLE_ASSIGNMENT (( #17297 ) ) ;
#3598=SURFACE_SIDE_STYLE ('',( #13189 ) ) ;
#3621=DIRECTION ( 'NONE',  ( 1.000000000000000000, 9.815121534730717399E-17, -0.000000000000000000 ) ) ;
#3629=( NAMED_UNIT ( * ) PLANE_ANGLE_UNIT ( ) SI_UNIT ( $, .RADIAN. ) );
#3632=VECTOR ( 'NONE', #13182, 1000.000000000000000 ) ;
#3644=VERTEX_POINT ( 'NONE', #17027 ) ;
#3662=VECTOR ( 'NONE', #3314, 1000.000000000000000 ) ;
#3663=DIRECTION ( 'NONE',  ( -1.000000000000000000, -9.815121534730717399E-17, 0.000000000000000000 ) ) ;
#3694=PLANE ( 'NONE',  #5111 ) ;
#3705=MECHANICAL_DESIGN_GEOMETRIC_PRESENTATION_REPRESENTATION('',(#12239),#15219);
#3709=FACE_OUTER_BOUND ( 'NONE', #3336, .T. ) ;
#3724=SURFACE_SIDE_STYLE ('',( #8548 ) ) ;
#3743=( LENGTH_UNIT ( ) NAMED_UNIT ( * ) SI_UNIT ( .MILLI., .METRE. ) );
#3760=ADVANCED_FACE ( 'NONE', ( #102 ), #12798, .F. ) ;
#3770=LINE ( 'NONE', #10148, #1244 ) ;
#3784=CIRCLE ( 'NONE', #18563, 2.000000000000001776 ) ;
#3813=VECTOR ( 'NONE', #15167, 1000.000000000000000 ) ;
#3843=LINE ( 'NONE', #16424, #17000 ) ;
#3867=PRESENTATION_STYLE_ASSIGNMENT (( #352 ) ) ;
#3884=CIRCLE ( 'NONE', #18995, 2.000000000000001776 ) ;
#3892=( LENGTH_UNIT ( ) NAMED_UNIT ( * ) SI_UNIT ( .MILLI., .METRE. ) );
#3895=( NAMED_UNIT ( * ) PLANE_ANGLE_UNIT ( ) SI_UNIT ( $, .RADIAN. ) );
#3902=ORIENTED_EDGE ( 'NONE', *, *, #17916, .T. ) ;
#3924=EDGE_LOOP ( 'NONE', ( #9913, #2396, #1039, #16592 ) ) ;
#3925=EDGE_LOOP ( 'NONE', ( #3081, #8088, #11459, #5820 ) ) ;
#3929=UNCERTAINTY_MEASURE_WITH_UNIT (LENGTH_MEASURE( 1.000000000000000082E-05 ), #10782, 'distance_accuracy_value', 'NONE');
#3946=VECTOR ( 'NONE', #11293, 1000.000000000000000 ) ;
#3954=CARTESIAN_POINT ( 'NONE',  ( 108.9893729001366154, 95.58236431990637527, 327.6194023386000822 ) ) ;
#3984=LINE ( 'NONE', #15019, #3632 ) ;
#3986=EDGE_CURVE ( 'NONE', #3644, #12074, #10711, .T. ) ;
#3995=( NAMED_UNIT ( * ) SI_UNIT ( $, .STERADIAN. ) SOLID_ANGLE_UNIT ( ) );
#4012=PRESENTATION_STYLE_ASSIGNMENT (( #811 ) ) ;
#4019=DIRECTION ( 'NONE',  ( 9.815121534730717399E-17, -1.000000000000000000, -0.000000000000000000 ) ) ;
#4033=AXIS2_PLACEMENT_3D ( 'NONE', #19731, #882, #1173 ) ;
#4037=LINE ( 'NONE', #14972, #16310 ) ;
#4054=SHAPE_REPRESENTATION ( 'Part14', ( #2741 ), #5024 ) ;
#4058=DIRECTION ( 'NONE',  ( -6.120180426682197225E-17, 0.6235460666509320404, -0.7817866094812263578 ) ) ;
#4060=VERTEX_POINT ( 'NONE', #4624 ) ;
#4072=ORIENTED_EDGE ( 'NONE', *, *, #13156, .T. ) ;
#4087=DIRECTION ( 'NONE',  ( -1.000000000000000000, -9.815121534730717399E-17, 0.000000000000000000 ) ) ;
#4095=STYLED_ITEM ( 'NONE', ( #11537 ), #538 ) ;
#4096=CARTESIAN_POINT ( 'NONE',  ( 111.4893729001366012, 127.7247684487574304, 250.0000000000000000 ) ) ;
#4122=( GEOMETRIC_REPRESENTATION_CONTEXT ( 3 ) GLOBAL_UNCERTAINTY_ASSIGNED_CONTEXT ( ( #15265 ) ) GLOBAL_UNIT_ASSIGNED_CONTEXT ( ( #2905, #10853, #1552 ) ) REPRESENTATION_CONTEXT ( 'NONE', 'WORKASPACE' ) );
#4124=STYLED_ITEM ( 'NONE', ( #9780 ), #15290 ) ;
#4128=( LENGTH_UNIT ( ) NAMED_UNIT ( * ) SI_UNIT ( .MILLI., .METRE. ) );
#4133=( NAMED_UNIT ( * ) SI_UNIT ( $, .STERADIAN. ) SOLID_ANGLE_UNIT ( ) );
#4137=DIRECTION ( 'NONE',  ( 9.815121534730717399E-17, -1.000000000000000000, 0.000000000000000000 ) ) ;
#4143=VECTOR ( 'NONE', #9536, 1000.000000000000114 ) ;
#4148=EDGE_CURVE ( 'NONE', #9009, #11794, #3884, .T. ) ;
#4162=( NAMED_UNIT ( * ) SI_UNIT ( $, .STERADIAN. ) SOLID_ANGLE_UNIT ( ) );
#4167=CARTESIAN_POINT ( 'NONE',  ( 108.9893729001366154, 131.2883416677199193, 282.8521325859589979 ) ) ;
#4178=UNCERTAINTY_MEASURE_WITH_UNIT (LENGTH_MEASURE( 1.000000000000000082E-05 ), #19450, 'distance_accuracy_value', 'NONE');
#4184=LINE ( 'NONE', #10450, #7504 ) ;
#4188=PRODUCT_CONTEXT ( 'NONE', #19331, 'mechanical' ) ;
#4217=APPLICATION_CONTEXT ( 'automotive_design' ) ;
#4225=CARTESIAN_POINT ( 'NONE',  ( 111.4893729001366012, 127.7247684487574588, 357.7985149490353933 ) ) ;
#4229=( LENGTH_UNIT ( ) NAMED_UNIT ( * ) SI_UNIT ( .MILLI., .METRE. ) );
#4275=DIRECTION ( 'NONE',  ( 0.000000000000000000, 1.000000000000000000, 0.000000000000000000 ) ) ;
#4278=AXIS2_PLACEMENT_3D ( 'NONE', #19130, #8132, #4834 ) ;
#4280=ORIENTED_EDGE ( 'NONE', *, *, #6579, .T. ) ;
#4292=( LENGTH_UNIT ( ) NAMED_UNIT ( * ) SI_UNIT ( .MILLI., .METRE. ) );
#4294=EDGE_CURVE ( 'NONE', #3644, #16358, #5447, .T. ) ;
#4319=FACE_OUTER_BOUND ( 'NONE', #8638, .T. ) ;
#4349=VERTEX_POINT ( 'NONE', #7196 ) ;
#4352=( GEOMETRIC_REPRESENTATION_CONTEXT ( 3 ) GLOBAL_UNCERTAINTY_ASSIGNED_CONTEXT ( ( #8275 ) ) GLOBAL_UNIT_ASSIGNED_CONTEXT ( ( #17482, #9776, #6381 ) ) REPRESENTATION_CONTEXT ( 'NONE', 'WORKASPACE' ) );
#4372=( NAMED_UNIT ( * ) SI_UNIT ( $, .STERADIAN. ) SOLID_ANGLE_UNIT ( ) );
#4386=DIRECTION ( 'NONE',  ( -9.815121534730717399E-17, 1.000000000000000000, 0.000000000000000000 ) ) ;
#4414=COLOUR_RGB ( '', 0.08235294, 0.09019608, 0.10196078) ;
#4436=ORIENTED_EDGE ( 'NONE', *, *, #9927, .T. ) ;
#4451=DIRECTION ( 'NONE',  ( 6.263247009234064878E-17, -0.6381222063396385646, 0.7699350945217602327 ) ) ;
#4466=CARTESIAN_POINT ( 'NONE',  ( 53.48937290013658696, 119.5973956464515879, 322.0399576098686225 ) ) ;
#4474=DIRECTION ( 'NONE',  ( -1.445602896647339163E-16, 1.000000000000000000, 0.000000000000000000 ) ) ;
#4477=DIRECTION ( 'NONE',  ( -1.000000000000000000, 0.000000000000000000, -0.000000000000000000 ) ) ;
#4484=VERTEX_POINT ( 'NONE', #15121 ) ;
#4495=LINE ( 'NONE', #10569, #13408 ) ;
#4502=SURFACE_STYLE_FILL_AREA ( #7799 ) ;
#4508=CARTESIAN_POINT ( 'NONE',  ( 53.48937290013659407, 129.7247684487574588, 283.6050404526570219 ) ) ;
#4512=SURFACE_STYLE_FILL_AREA ( #15547 ) ;
#4521=LINE ( 'NONE', #274, #15976 ) ;
#4605=LINE ( 'NONE', #4508, #4143 ) ;
#4608=DIRECTION ( 'NONE',  ( 0.000000000000000000, 1.000000000000000000, 0.000000000000000000 ) ) ;
#4624=CARTESIAN_POINT ( 'NONE',  ( 55.98937290013660117, 131.2883416677198625, 282.8521325859588842 ) ) ;
#4636=VERTEX_POINT ( 'NONE', #16063 ) ;
#4643=( GEOMETRIC_REPRESENTATION_CONTEXT ( 3 ) GLOBAL_UNCERTAINTY_ASSIGNED_CONTEXT ( ( #18542 ) ) GLOBAL_UNIT_ASSIGNED_CONTEXT ( ( #9073, #15462, #9161 ) ) REPRESENTATION_CONTEXT ( 'NONE', 'WORKASPACE' ) );
#4648=FILL_AREA_STYLE_COLOUR ( '', #19186 ) ;
#4658=ADVANCED_FACE ( 'NONE', ( #1893 ), #6562, .T. ) ;
#4667=FACE_OUTER_BOUND ( 'NONE', #17355, .T. ) ;
#4684=AXIS2_PLACEMENT_3D ( 'NONE', #4836, #279, #5038 ) ;
#4705=DIRECTION ( 'NONE',  ( 0.000000000000000000, -0.6381222063396385646, 0.7699350945217602327 ) ) ;
#4707=VERTEX_POINT ( 'NONE', #754 ) ;
#4732=VECTOR ( 'NONE', #9060, 1000.000000000000000 ) ;
#4761=( GEOMETRIC_REPRESENTATION_CONTEXT ( 3 ) GLOBAL_UNCERTAINTY_ASSIGNED_CONTEXT ( ( #749 ) ) GLOBAL_UNIT_ASSIGNED_CONTEXT ( ( #9296, #15910, #6430 ) ) REPRESENTATION_CONTEXT ( 'NONE', 'WORKASPACE' ) );
#4767=VECTOR ( 'NONE', #14917, 1000.000000000000000 ) ;
#4774=( GEOMETRIC_REPRESENTATION_CONTEXT ( 3 ) GLOBAL_UNCERTAINTY_ASSIGNED_CONTEXT ( ( #2286 ) ) GLOBAL_UNIT_ASSIGNED_CONTEXT ( ( #1502, #1385, #7816 ) ) REPRESENTATION_CONTEXT ( 'NONE', 'WORKASPACE' ) );
#4799=COLOUR_RGB ( '', 0.31764706, 0.68627451, 0.89019608) ;
#4812=SURFACE_STYLE_USAGE ( .BOTH. , #12532 ) ;
#4816=DIRECTION ( 'NONE',  ( -1.000000000000000000, -1.694044051971171780E-15, -1.283989322801278906E-15 ) ) ;
#4831=SURFACE_STYLE_USAGE ( .BOTH. , #15668 ) ;
#4834=DIRECTION ( 'NONE',  ( 0.000000000000000000, 1.000000000000000000, 0.000000000000000000 ) ) ;
#4836=CARTESIAN_POINT ( 'NONE',  ( 55.48937290013660117, 127.7247684487574304, 368.0000000000000000 ) ) ;
#4837=( NAMED_UNIT ( * ) PLANE_ANGLE_UNIT ( ) SI_UNIT ( $, .RADIAN. ) );
#4874=PRESENTATION_STYLE_ASSIGNMENT (( #8070 ) ) ;
#4900=FILL_AREA_STYLE ('',( #17364 ) ) ;
#4915=FILL_AREA_STYLE ('',( #12540 ) ) ;
#4926=SURFACE_STYLE_FILL_AREA ( #18928 ) ;
#4938=LINE ( 'NONE', #6291, #9516 ) ;
#4939=EDGE_LOOP ( 'NONE', ( #11663, #5023, #14110, #18715 ) ) ;
#4958=DIRECTION ( 'NONE',  ( -8.188278247072579902E-16, 0.7817866094812263578, 0.6235460666509320404 ) ) ;
#4999=( GEOMETRIC_REPRESENTATION_CONTEXT ( 3 ) GLOBAL_UNCERTAINTY_ASSIGNED_CONTEXT ( ( #16918 ) ) GLOBAL_UNIT_ASSIGNED_CONTEXT ( ( #3480, #360, #4372 ) ) REPRESENTATION_CONTEXT ( 'NONE', 'WORKASPACE' ) );
#5007=FACE_OUTER_BOUND ( 'NONE', #3143, .T. ) ;
#5023=ORIENTED_EDGE ( 'NONE', *, *, #13393, .T. ) ;
#5024=( GEOMETRIC_REPRESENTATION_CONTEXT ( 3 ) GLOBAL_UNCERTAINTY_ASSIGNED_CONTEXT ( ( #16485 ) ) GLOBAL_UNIT_ASSIGNED_CONTEXT ( ( #17685, #14786, #10062 ) ) REPRESENTATION_CONTEXT ( 'NONE', 'WORKASPACE' ) );
#5036=ORIENTED_EDGE ( 'NONE', *, *, #11142, .T. ) ;
#5038=DIRECTION ( 'NONE',  ( 1.000000000000000000, 0.000000000000000000, 0.000000000000000000 ) ) ;
#5041=DIRECTION ( 'NONE',  ( -9.815121534730717399E-17, 1.000000000000000000, -2.352167425053297897E-16 ) ) ;
#5042=CARTESIAN_POINT ( 'NONE',  ( 0.000000000000000000, 0.000000000000000000, 0.000000000000000000 ) ) ;
#5052=MECHANICAL_DESIGN_GEOMETRIC_PRESENTATION_REPRESENTATION('',(#2392),#10307);
#5071=CARTESIAN_POINT ( 'NONE',  ( 53.48937290013658696, 126.1646452518344859, 322.0399576098686225 ) ) ;
#5077=( NAMED_UNIT ( * ) SI_UNIT ( $, .STERADIAN. ) SOLID_ANGLE_UNIT ( ) );
#5095=FILL_AREA_STYLE_COLOUR ( '', #3274 ) ;
#5111=AXIS2_PLACEMENT_3D ( 'NONE', #8445, #14409, #14613 ) ;
#5113=ADVANCED_FACE ( 'NONE', ( #14673, #8569, #14867 ), #19194, .T. ) ;
#5117=EDGE_LOOP ( 'NONE', ( #5596, #16541, #19394, #14597, #18988, #14183, #16328, #13903, #670, #8410, #7186, #11478 ) ) ;
#5122=VECTOR ( 'NONE', #9524, 1000.000000000000000 ) ;
#5142=AXIS2_PLACEMENT_3D ( 'NONE', #2423, #20312, #18081 ) ;
#5154=CARTESIAN_POINT ( 'NONE',  ( 55.48937290013660117, 129.7247684487574588, 368.0000000000000000 ) ) ;
#5189=UNCERTAINTY_MEASURE_WITH_UNIT (LENGTH_MEASURE( 1.000000000000000082E-05 ), #19529, 'distance_accuracy_value', 'NONE');
#5197=SURFACE_STYLE_FILL_AREA ( #17953 ) ;
#5211=UNCERTAINTY_MEASURE_WITH_UNIT (LENGTH_MEASURE( 1.000000000000000082E-05 ), #3522, 'distance_accuracy_value', 'NONE');
#5216=CYLINDRICAL_SURFACE ( 'NONE', #15237, 2.000000000000001776 ) ;
#5224=SHAPE_REPRESENTATION_RELATIONSHIP ( 'NONE' , 'NONE' ,  #4054, #17238 ) ;
#5241=CARTESIAN_POINT ( 'NONE',  ( 111.4893729001366012, 129.7247684487574588, 368.0000000000000000 ) ) ;
#5246=FACE_OUTER_BOUND ( 'NONE', #1343, .T. ) ;
#5283=AXIS2_PLACEMENT_3D ( 'NONE', #2508, #19794, #5703 ) ;
#5317=DIRECTION ( 'NONE',  ( 1.000000000000000000, 9.815121534730717399E-17, 0.000000000000000000 ) ) ;
#5357=FACE_BOUND ( 'NONE', #3925, .T. ) ;
#5374=EDGE_CURVE ( 'NONE', #7754, #10337, #19535, .T. ) ;
#5410=ORIENTED_EDGE ( 'NONE', *, *, #2351, .T. ) ;
#5447=LINE ( 'NONE', #8335, #17365 ) ;
#5450=STYLED_ITEM ( 'NONE', ( #11890 ), #2091 ) ;
#5464=SURFACE_STYLE_USAGE ( .BOTH. , #8352 ) ;
#5469=DIRECTION ( 'NONE',  ( 0.000000000000000000, 0.000000000000000000, 1.000000000000000000 ) ) ;
#5485=ORIENTED_EDGE ( 'NONE', *, *, #1098, .T. ) ;
#5505=EDGE_CURVE ( 'NONE', #18128, #2161, #10184, .T. ) ;
#5530=PLANE ( 'NONE',  #5142 ) ;
#5535=PLANE ( 'NONE',  #6596 ) ;
#5542=FILL_AREA_STYLE ('',( #15029 ) ) ;
#5554=DIRECTION ( 'NONE',  ( 1.000000000000000000, 9.815121534730717399E-17, 0.000000000000000000 ) ) ;
#5558=DIRECTION ( 'NONE',  ( 1.000000000000000000, 9.815121534730718631E-17, 0.000000000000000000 ) ) ;
#5564=DIRECTION ( 'NONE',  ( 0.000000000000000000, -0.5937146717273790175, -0.8046756418431283420 ) ) ;
#5587=PRESENTATION_STYLE_ASSIGNMENT (( #5999 ) ) ;
#5591=EDGE_CURVE ( 'NONE', #12975, #14376, #2936, .T. ) ;
#5596=ORIENTED_EDGE ( 'NONE', *, *, #14940, .F. ) ;
#5630=SURFACE_STYLE_FILL_AREA ( #19717 ) ;
#5632=VERTEX_POINT ( 'NONE', #14775 ) ;
#5645=SURFACE_STYLE_USAGE ( .BOTH. , #15031 ) ;
#5655=CARTESIAN_POINT ( 'NONE',  ( 111.4893729001366012, 122.8810204491430369, 322.0399576098686225 ) ) ;
#5664=FACE_OUTER_BOUND ( 'NONE', #5117, .T. ) ;
#5677=COLOUR_RGB ( '', 0.66274510, 0.83137255, 0.94901961) ;
#5686=LINE ( 'NONE', #8878, #18178 ) ;
#5701=EDGE_CURVE ( 'NONE', #2573, #10931, #8409, .T. ) ;
#5703=DIRECTION ( 'NONE',  ( 0.000000000000000000, 1.000000000000000000, 0.000000000000000000 ) ) ;
#5727=COLOUR_RGB ( '', 0.72549020, 0.75294118, 0.79215686) ;
#5730=STYLED_ITEM ( 'NONE', ( #2462 ), #8010 ) ;
#5757=ORIENTED_EDGE ( 'NONE', *, *, #11793, .F. ) ;
#5778=COLOUR_RGB ( '', 0.66274510, 0.83137255, 0.94901961) ;
#5812=UNCERTAINTY_MEASURE_WITH_UNIT (LENGTH_MEASURE( 1.000000000000000082E-05 ), #4128, 'distance_accuracy_value', 'NONE');
#5820=ORIENTED_EDGE ( 'NONE', *, *, #5701, .T. ) ;
#5885=ORIENTED_EDGE ( 'NONE', *, *, #17605, .T. ) ;
#5908=CARTESIAN_POINT ( 'NONE',  ( 53.48937290013659407, 125.7247684487574588, 252.0000000000000000 ) ) ;
#5921=STYLED_ITEM ( 'NONE', ( #7099 ), #6762 ) ;
#5922=EDGE_CURVE ( 'NONE', #10337, #12769, #10537, .T. ) ;
#5929=ORIENTED_EDGE ( 'NONE', *, *, #19943, .F. ) ;
#5945=PLANE ( 'NONE',  #2010 ) ;
#5950=ORIENTED_EDGE ( 'NONE', *, *, #5505, .F. ) ;
#5953=VECTOR ( 'NONE', #16113, 1000.000000000000000 ) ;
#5964=CARTESIAN_POINT ( 'NONE',  ( 111.4893729001366012, 129.7247684487574588, 283.6050404526570219 ) ) ;
#5972=FILL_AREA_STYLE ('',( #9258 ) ) ;
#5975=MECHANICAL_DESIGN_GEOMETRIC_PRESENTATION_REPRESENTATION('',(#12220),#4999);
#5983=EDGE_CURVE ( 'NONE', #7678, #6221, #15610, .T. ) ;
#5999=SURFACE_STYLE_USAGE ( .BOTH. , #11885 ) ;
#6072=SURFACE_STYLE_FILL_AREA ( #893 ) ;
#6092=ORIENTED_EDGE ( 'NONE', *, *, #9345, .T. ) ;
#6095=MECHANICAL_DESIGN_GEOMETRIC_PRESENTATION_REPRESENTATION('',(#7403),#14634);
#6109=LINE ( 'NONE', #18660, #11675 ) ;
#6118=COLOUR_RGB ( '', 0.66274510, 0.83137255, 0.94901961) ;
#6124=SURFACE_SIDE_STYLE ('',( #18767 ) ) ;
#6134=CARTESIAN_POINT ( 'NONE',  ( 111.4893729001366012, 129.7247684487574304, 252.0000000000000000 ) ) ;
#6136=LINE ( 'NONE', #9307, #17932 ) ;
#6137=VERTEX_POINT ( 'NONE', #6844 ) ;
#6157=FILL_AREA_STYLE_COLOUR ( '', #8545 ) ;
#6201=CARTESIAN_POINT ( 'NONE',  ( 53.48937290013659407, 129.7247684487574588, 368.0000000000000000 ) ) ;
#6219=CARTESIAN_POINT ( 'NONE',  ( 55.48937290013659407, 208.2413221699789858, 346.7388812057777727 ) ) ;
#6221=VERTEX_POINT ( 'NONE', #11976 ) ;
#6279=CARTESIAN_POINT ( 'NONE',  ( 111.4893729001366012, 125.7247684487574588, 252.0000000000000000 ) ) ;
#6291=CARTESIAN_POINT ( 'NONE',  ( 111.4893729001366012, 127.7247684487574588, 254.0000000000000000 ) ) ;
#6298=DIRECTION ( 'NONE',  ( -9.815121534730717399E-17, 1.000000000000000000, 0.000000000000000000 ) ) ;
#6314=( LENGTH_UNIT ( ) NAMED_UNIT ( * ) SI_UNIT ( .MILLI., .METRE. ) );
#6322=( NAMED_UNIT ( * ) SI_UNIT ( $, .STERADIAN. ) SOLID_ANGLE_UNIT ( ) );
#6344=STYLED_ITEM ( 'NONE', ( #11204 ), #3060 ) ;
#6359=( LENGTH_UNIT ( ) NAMED_UNIT ( * ) SI_UNIT ( .MILLI., .METRE. ) );
#6366=SURFACE_STYLE_USAGE ( .BOTH. , #1491 ) ;
#6381=( NAMED_UNIT ( * ) SI_UNIT ( $, .STERADIAN. ) SOLID_ANGLE_UNIT ( ) );
#6387=CIRCLE ( 'NONE', #8998, 3.283624802691453848 ) ;
#6402=AXIS2_PLACEMENT_3D ( 'NONE', #20168, #10915, #1393 ) ;
#6406=LINE ( 'NONE', #12694, #18564 ) ;
#6430=( NAMED_UNIT ( * ) SI_UNIT ( $, .STERADIAN. ) SOLID_ANGLE_UNIT ( ) );
#6446=VERTEX_POINT ( 'NONE', #19857 ) ;
#6468=( NAMED_UNIT ( * ) SI_UNIT ( $, .STERADIAN. ) SOLID_ANGLE_UNIT ( ) );
#6475=ORIENTED_EDGE ( 'NONE', *, *, #18968, .T. ) ;
#6481=FILL_AREA_STYLE ('',( #14195 ) ) ;
#6527=DIRECTION ( 'NONE',  ( -1.000000000000000000, -9.815121534730717399E-17, 0.000000000000000000 ) ) ;
#6533=FILL_AREA_STYLE_COLOUR ( '', #13983 ) ;
#6546=ORIENTED_EDGE ( 'NONE', *, *, #2082, .F. ) ;
#6562=PLANE ( 'NONE',  #9478 ) ;
#6579=EDGE_CURVE ( 'NONE', #8530, #10337, #16901, .T. ) ;
#6596=AXIS2_PLACEMENT_3D ( 'NONE', #6897, #8518, #18088 ) ;
#6626=FILL_AREA_STYLE ('',( #11352 ) ) ;
#6628=EDGE_CURVE ( 'NONE', #4484, #693, #10196, .T. ) ;
#6629=LINE ( 'NONE', #11355, #3662 ) ;
#6633=ORIENTED_EDGE ( 'NONE', *, *, #11655, .F. ) ;
#6644=VERTEX_POINT ( 'NONE', #14403 ) ;
#6679=AXIS2_PLACEMENT_3D ( 'NONE', #18089, #14607, #19527 ) ;
#6701=VECTOR ( 'NONE', #4816, 1000.000000000000000 ) ;
#6702=FILL_AREA_STYLE_COLOUR ( '', #6118 ) ;
#6711=SURFACE_STYLE_FILL_AREA ( #16201 ) ;
#6734=ORIENTED_EDGE ( 'NONE', *, *, #19425, .T. ) ;
#6737=EDGE_LOOP ( 'NONE', ( #13402, #573, #16102, #9549 ) ) ;
#6750=VECTOR ( 'NONE', #19226, 1000.000000000000000 ) ;
#6762=ADVANCED_FACE ( 'NONE', ( #8735 ), #5535, .T. ) ;
#6780=EDGE_CURVE ( 'NONE', #19519, #10459, #3984, .T. ) ;
#6792=( GEOMETRIC_REPRESENTATION_CONTEXT ( 3 ) GLOBAL_UNCERTAINTY_ASSIGNED_CONTEXT ( ( #3537 ) ) GLOBAL_UNIT_ASSIGNED_CONTEXT ( ( #6314, #12291, #6322 ) ) REPRESENTATION_CONTEXT ( 'NONE', 'WORKASPACE' ) );
#6800=PRESENTATION_STYLE_ASSIGNMENT (( #14912 ) ) ;
#6829=FILL_AREA_STYLE ('',( #14432 ) ) ;
#6833=EDGE_CURVE ( 'NONE', #10459, #7754, #2430, .T. ) ;
#6844=CARTESIAN_POINT ( 'NONE',  ( 111.4893729001366012, 126.1646452518344859, 322.0399576098686225 ) ) ;
#6853=CARTESIAN_POINT ( 'NONE',  ( 111.4893729001366012, 119.5973956464515879, 280.0825295754780768 ) ) ;
#6858=EDGE_CURVE ( 'NONE', #18127, #19519, #11925, .T. ) ;
#6884=STYLED_ITEM ( 'NONE', ( #1579 ), #4658 ) ;
#6894=FILL_AREA_STYLE_COLOUR ( '', #7320 ) ;
#6897=CARTESIAN_POINT ( 'NONE',  ( 111.4893729001366012, 127.7247684487574304, 250.0000000000000000 ) ) ;
#6908=CARTESIAN_POINT ( 'NONE',  ( 108.9893729001365870, 144.5787140289007766, 293.4524157190248275 ) ) ;
#6916=ADVANCED_FACE ( 'NONE', ( #16977 ), #20134, .T. ) ;
#6918=DIRECTION ( 'NONE',  ( 0.000000000000000000, -0.7791332379872890623, -0.6268583551835633649 ) ) ;
#6927=COLOUR_RGB ( '', 0.72549020, 0.75294118, 0.79215686) ;
#6928=( GEOMETRIC_REPRESENTATION_CONTEXT ( 3 ) GLOBAL_UNCERTAINTY_ASSIGNED_CONTEXT ( ( #15289 ) ) GLOBAL_UNIT_ASSIGNED_CONTEXT ( ( #4292, #2836, #12212 ) ) REPRESENTATION_CONTEXT ( 'NONE', 'WORKASPACE' ) );
#6991=LINE ( 'NONE', #10381, #11688 ) ;
#6999=CARTESIAN_POINT ( 'NONE',  ( 53.48937290013660117, 77.72476844875745883, 252.0000000000000000 ) ) ;
#7015=( NAMED_UNIT ( * ) SI_UNIT ( $, .STERADIAN. ) SOLID_ANGLE_UNIT ( ) );
#7026=LINE ( 'NONE', #18024, #5953 ) ;
#7028=( LENGTH_UNIT ( ) NAMED_UNIT ( * ) SI_UNIT ( .MILLI., .METRE. ) );
#7033=ORIENTED_EDGE ( 'NONE', *, *, #5591, .F. ) ;
#7041=CARTESIAN_POINT ( 'NONE',  ( 111.4893729001366012, 129.7247684487574588, 283.6050404526570219 ) ) ;
#7049=EDGE_CURVE ( 'NONE', #9009, #9433, #8644, .T. ) ;
#7057=VECTOR ( 'NONE', #6527, 1000.000000000000000 ) ;
#7073=ORIENTED_EDGE ( 'NONE', *, *, #17916, .F. ) ;
#7099=PRESENTATION_STYLE_ASSIGNMENT (( #19628 ) ) ;
#7152=EDGE_CURVE ( 'NONE', #6221, #6137, #19737, .T. ) ;
#7156=( LENGTH_UNIT ( ) NAMED_UNIT ( * ) SI_UNIT ( .MILLI., .METRE. ) );
#7157=DIRECTION ( 'NONE',  ( -6.120180426682197225E-17, 0.6235460666509320404, -0.7817866094812263578 ) ) ;
#7186=ORIENTED_EDGE ( 'NONE', *, *, #7255, .T. ) ;
#7196=CARTESIAN_POINT ( 'NONE',  ( 53.48937290013662249, 49.66333933884487806, 252.0000000000000000 ) ) ;
#7200=FACE_OUTER_BOUND ( 'NONE', #13755, .T. ) ;
#7231=ORIENTED_EDGE ( 'NONE', *, *, #16090, .T. ) ;
#7255=EDGE_CURVE ( 'NONE', #12831, #889, #3533, .T. ) ;
#7284=VECTOR ( 'NONE', #9495, 1000.000000000000000 ) ;
#7306=VECTOR ( 'NONE', #19236, 1000.000000000000000 ) ;
#7313=SURFACE_STYLE_USAGE ( .BOTH. , #18420 ) ;
#7320=COLOUR_RGB ( '', 0.72549020, 0.75294118, 0.79215686) ;
#7353=EDGE_CURVE ( 'NONE', #12074, #1376, #6629, .T. ) ;
#7386=DIRECTION ( 'NONE',  ( -0.000000000000000000, 0.7817866094812239153, 0.6235460666509350380 ) ) ;
#7402=PRESENTATION_STYLE_ASSIGNMENT (( #12047 ) ) ;
#7403=STYLED_ITEM ( 'NONE', ( #818 ), #16014 ) ;
#7409=COLOUR_RGB ( '', 0.66274510, 0.83137255, 0.94901961) ;
#7411=PRODUCT_DEFINITION_CONTEXT ( 'detailed design', #4217, 'design' ) ;
#7412=MECHANICAL_DESIGN_GEOMETRIC_PRESENTATION_REPRESENTATION('',(#12035),#16316);
#7481=ORIENTED_EDGE ( 'NONE', *, *, #4294, .T. ) ;
#7490=EDGE_CURVE ( 'NONE', #889, #2901, #10319, .T. ) ;
#7504=VECTOR ( 'NONE', #16757, 1000.000000000000000 ) ;
#7534=CARTESIAN_POINT ( 'NONE',  ( 111.4893729001366012, 127.7247684487574304, 252.0000000000000000 ) ) ;
#7582=SURFACE_STYLE_FILL_AREA ( #4900 ) ;
#7593=DIRECTION ( 'NONE',  ( 1.000000000000000000, 9.815121534730717399E-17, 0.000000000000000000 ) ) ;
#7627=VERTEX_POINT ( 'NONE', #8870 ) ;
#7650=SURFACE_SIDE_STYLE ('',( #5630 ) ) ;
#7664=SURFACE_STYLE_USAGE ( .BOTH. , #1459 ) ;
#7665=CARTESIAN_POINT ( 'NONE',  ( 111.4893729001366012, 209.4935875941501422, 345.2279431939882670 ) ) ;
#7678=VERTEX_POINT ( 'NONE', #12383 ) ;
#7680=ORIENTED_EDGE ( 'NONE', *, *, #18968, .F. ) ;
#7684=PRESENTATION_STYLE_ASSIGNMENT (( #151 ) ) ;
#7690=FILL_AREA_STYLE_COLOUR ( '', #4414 ) ;
#7700=( NAMED_UNIT ( * ) PLANE_ANGLE_UNIT ( ) SI_UNIT ( $, .RADIAN. ) );
#7713=FACE_OUTER_BOUND ( 'NONE', #15742, .T. ) ;
#7725=MECHANICAL_DESIGN_GEOMETRIC_PRESENTATION_REPRESENTATION('',(#8712),#4774);
#7740=CARTESIAN_POINT ( 'NONE',  ( 55.48937290013659407, 211.0574367717017594, 346.4752554294135507 ) ) ;
#7754=VERTEX_POINT ( 'NONE', #9794 ) ;
#7760=( GEOMETRIC_REPRESENTATION_CONTEXT ( 3 ) GLOBAL_UNCERTAINTY_ASSIGNED_CONTEXT ( ( #19032 ) ) GLOBAL_UNIT_ASSIGNED_CONTEXT ( ( #13935, #12402, #2898 ) ) REPRESENTATION_CONTEXT ( 'NONE', 'WORKASPACE' ) );
#7782=PRODUCT_DEFINITION_SHAPE ( 'NONE', 'NONE',  #9349 ) ;
#7784=CARTESIAN_POINT ( 'NONE',  ( 53.48937290013659407, 127.7247684487574304, 250.0000000000000000 ) ) ;
#7799=FILL_AREA_STYLE ('',( #7690 ) ) ;
#7809=ORIENTED_EDGE ( 'NONE', *, *, #16906, .F. ) ;
#7816=( NAMED_UNIT ( * ) SI_UNIT ( $, .STERADIAN. ) SOLID_ANGLE_UNIT ( ) );
#7824=CARTESIAN_POINT ( 'NONE',  ( 54.31780002488277148, 209.7811923590225547, 348.0151256184570343 ) ) ;
#7833=ORIENTED_EDGE ( 'NONE', *, *, #3986, .T. ) ;
#7834=DIRECTION ( 'NONE',  ( -1.000000000000000000, -9.815121534730717399E-17, 0.000000000000000000 ) ) ;
#7911=ORIENTED_EDGE ( 'NONE', *, *, #10396, .F. ) ;
#7917=( NAMED_UNIT ( * ) SI_UNIT ( $, .STERADIAN. ) SOLID_ANGLE_UNIT ( ) );
#7925=DIRECTION ( 'NONE',  ( -1.000000000000000000, -9.815121534730717399E-17, 0.000000000000000000 ) ) ;
#7933=VERTEX_POINT ( 'NONE', #1186 ) ;
#7956=STYLED_ITEM ( 'NONE', ( #11935 ), #17542 ) ;
#7976=EDGE_CURVE ( 'NONE', #10796, #19149, #10405, .T. ) ;
#7981=VERTEX_POINT ( 'NONE', #12065 ) ;
#8010=ADVANCED_FACE ( 'NONE', ( #10704 ), #16708, .F. ) ;
#8018=AXIS2_PLACEMENT_3D ( 'NONE', #8544, #4137, #901 ) ;
#8041=( GEOMETRIC_REPRESENTATION_CONTEXT ( 3 ) GLOBAL_UNCERTAINTY_ASSIGNED_CONTEXT ( ( #13032 ) ) GLOBAL_UNIT_ASSIGNED_CONTEXT ( ( #3743, #16232, #13230 ) ) REPRESENTATION_CONTEXT ( 'NONE', 'WORKASPACE' ) );
#8048=( LENGTH_UNIT ( ) NAMED_UNIT ( * ) SI_UNIT ( .MILLI., .METRE. ) );
#8070=SURFACE_STYLE_USAGE ( .BOTH. , #6124 ) ;
#8087=COLOUR_RGB ( '', 0.09019608, 0.27058824, 0.51372549) ;
#8088=ORIENTED_EDGE ( 'NONE', *, *, #18752, .T. ) ;
#8112=CARTESIAN_POINT ( 'NONE',  ( 110.6609457753904024, 209.7811923590225263, 348.0151256184569775 ) ) ;
#8119=ADVANCED_FACE ( 'NONE', ( #7713 ), #19016, .F. ) ;
#8132=DIRECTION ( 'NONE',  ( 1.000000000000000000, 9.815121534730717399E-17, 0.000000000000000000 ) ) ;
#8165=DIRECTION ( 'NONE',  ( 1.000000000000000000, 9.815121534730718631E-17, -0.000000000000000000 ) ) ;
#8166=MANIFOLD_SOLID_BREP ( 'Cut-Extrude7', #1063 ) ;
#8175=EDGE_LOOP ( 'NONE', ( #7809, #6633, #10137, #17783 ) ) ;
#8208=SURFACE_SIDE_STYLE ('',( #15751 ) ) ;
#8214=CARTESIAN_POINT ( 'NONE',  ( -77.99033078109007988, 125.7247684487574304, 254.0000000000000000 ) ) ;
#8217=ORIENTED_EDGE ( 'NONE', *, *, #2449, .T. ) ;
#8225=( LENGTH_UNIT ( ) NAMED_UNIT ( * ) SI_UNIT ( .MILLI., .METRE. ) );
#8234=DIRECTION ( 'NONE',  ( 1.000000000000000000, 0.000000000000000000, 0.000000000000000000 ) ) ;
#8261=MANIFOLD_SOLID_BREP ( 'Fillet1', #1387 ) ;
#8275=UNCERTAINTY_MEASURE_WITH_UNIT (LENGTH_MEASURE( 1.000000000000000082E-05 ), #17482, 'distance_accuracy_value', 'NONE');
#8282=SURFACE_STYLE_FILL_AREA ( #9412 ) ;
#8299=UNCERTAINTY_MEASURE_WITH_UNIT (LENGTH_MEASURE( 1.000000000000000082E-05 ), #6359, 'distance_accuracy_value', 'NONE');
#8324=COLOUR_RGB ( '', 0.40784314, 0.44705882, 0.49803922) ;
#8327=CARTESIAN_POINT ( 'NONE',  ( 111.4893729001366012, 208.2227610943810134, 346.7612763259490407 ) ) ;
#8335=CARTESIAN_POINT ( 'NONE',  ( 53.48937290013659407, 129.7247684487574588, 370.0000000000000000 ) ) ;
#8344=VERTEX_POINT ( 'NONE', #651 ) ;
#8352=SURFACE_SIDE_STYLE ('',( #6711 ) ) ;
#8358=CARTESIAN_POINT ( 'NONE',  ( 108.9893729001365870, 108.8727366810872468, 338.2196854716659118 ) ) ;
#8364=( NAMED_UNIT ( * ) PLANE_ANGLE_UNIT ( ) SI_UNIT ( $, .RADIAN. ) );
#8368=VECTOR ( 'NONE', #4474, 1000.000000000000000 ) ;
#8374=AXIS2_PLACEMENT_3D ( 'NONE', #2458, #16306, #6918 ) ;
#8383=STYLED_ITEM ( 'NONE', ( #2537 ), #12423 ) ;
#8384=VECTOR ( 'NONE', #8165, 1000.000000000000000 ) ;
#8388=CARTESIAN_POINT ( 'NONE',  ( 111.4893729001366154, 49.66333933884488516, 252.0000000000000000 ) ) ;
#8402=ADVANCED_FACE ( 'NONE', ( #5007 ), #5216, .F. ) ;
#8409=LINE ( 'NONE', #2092, #8876 ) ;
#8410=ORIENTED_EDGE ( 'NONE', *, *, #18313, .T. ) ;
#8413=DIRECTION ( 'NONE',  ( 0.000000000000000000, -1.000000000000000000, 0.000000000000000000 ) ) ;
#8415=AXIS2_PLACEMENT_3D ( 'NONE', #3383, #14608, #12773 ) ;
#8427=ORIENTED_EDGE ( 'NONE', *, *, #5505, .T. ) ;
#8445=CARTESIAN_POINT ( 'NONE',  ( 111.4893729001366012, 129.7247684487574588, 370.0000000000000000 ) ) ;
#8461=CARTESIAN_POINT ( 'NONE',  ( 111.4893729001365728, 210.4096692328539007, 345.9586017849864561 ) ) ;
#8495=CARTESIAN_POINT ( 'NONE',  ( 111.4893729001366012, 122.8810204491430369, 280.0825295754780768 ) ) ;
#8518=DIRECTION ( 'NONE',  ( 0.000000000000000000, 0.000000000000000000, -1.000000000000000000 ) ) ;
#8530=VERTEX_POINT ( 'NONE', #11101 ) ;
#8544=CARTESIAN_POINT ( 'NONE',  ( 109.4893729001366012, 127.7247684487574588, 368.0000000000000000 ) ) ;
#8545=COLOUR_RGB ( '', 0.40784314, 0.44705882, 0.49803922) ;
#8548=SURFACE_STYLE_FILL_AREA ( #11762 ) ;
#8569=FACE_BOUND ( 'NONE', #9050, .T. ) ;
#8608=ORIENTED_EDGE ( 'NONE', *, *, #4294, .F. ) ;
#8615=SURFACE_SIDE_STYLE ('',( #19426 ) ) ;
#8634=CIRCLE ( 'NONE', #9962, 3.283624802691453848 ) ;
#8638=EDGE_LOOP ( 'NONE', ( #8217, #4436, #5929, #2568 ) ) ;
#8644=LINE ( 'NONE', #14733, #2294 ) ;
#8647=STYLED_ITEM ( 'NONE', ( #2178 ), #11440 ) ;
#8652=FILL_AREA_STYLE_COLOUR ( '', #5727 ) ;
#8661=EDGE_CURVE ( 'NONE', #7678, #16895, #14212, .T. ) ;
#8697=STYLED_ITEM ( 'NONE', ( #10678 ), #12465 ) ;
#8712=STYLED_ITEM ( 'NONE', ( #1702 ), #808 ) ;
#8726=ORIENTED_EDGE ( 'NONE', *, *, #7152, .T. ) ;
#8735=FACE_OUTER_BOUND ( 'NONE', #17174, .T. ) ;
#8747=DIRECTION ( 'NONE',  ( -1.445602896647339163E-16, 1.000000000000000000, 0.000000000000000000 ) ) ;
#8748=SURFACE_STYLE_FILL_AREA ( #15342 ) ;
#8765=ADVANCED_FACE ( 'NONE', ( #13474 ), #5530, .F. ) ;
#8794=CARTESIAN_POINT ( 'NONE',  ( 55.98937290013660828, 108.8727366810871899, 338.2196854716659118 ) ) ;
#8833=DIRECTION ( 'NONE',  ( 1.055507992432142416E-16, -0.5937146717273791285, -0.8046756418431282309 ) ) ;
#8834=EDGE_CURVE ( 'NONE', #5632, #1294, #11054, .T. ) ;
#8870=CARTESIAN_POINT ( 'NONE',  ( 53.48937290013659407, 127.7247684487574588, 368.0000000000000000 ) ) ;
#8876=VECTOR ( 'NONE', #11585, 1000.000000000000000 ) ;
#8878=CARTESIAN_POINT ( 'NONE',  ( 111.4893729001366012, 127.7247684487574304, 250.0000000000000000 ) ) ;
#8887=VECTOR ( 'NONE', #13568, 1000.000000000000000 ) ;
#8888=VECTOR ( 'NONE', #1641, 1000.000000000000000 ) ;
#8893=CARTESIAN_POINT ( 'NONE',  ( 53.48937290013658696, 122.8810204491430369, 280.0825295754780768 ) ) ;
#8917=ORIENTED_EDGE ( 'NONE', *, *, #10213, .T. ) ;
#8925=CARTESIAN_POINT ( 'NONE',  ( 108.9893729001366154, 95.58236431990637527, 327.6194023386000822 ) ) ;
#8933=ORIENTED_EDGE ( 'NONE', *, *, #6780, .T. ) ;
#8946=DIRECTION ( 'NONE',  ( 1.000000000000000000, 9.815121534730717399E-17, 0.000000000000000000 ) ) ;
#8950=CARTESIAN_POINT ( 'NONE',  ( 111.4893729001366012, 127.7247684487574304, 252.0000000000000000 ) ) ;
#8958=CIRCLE ( 'NONE', #6679, 3.283624802691453848 ) ;
#8963=DIRECTION ( 'NONE',  ( 0.000000000000000000, 1.000000000000000000, 0.000000000000000000 ) ) ;
#8974=STYLED_ITEM ( 'NONE', ( #3867 ), #8402 ) ;
#8998=AXIS2_PLACEMENT_3D ( 'NONE', #2520, #16852, #4275 ) ;
#9009=VERTEX_POINT ( 'NONE', #15832 ) ;
#9010=DIRECTION ( 'NONE',  ( 9.815121534730717399E-17, -1.000000000000000000, 0.000000000000000000 ) ) ;
#9043=FACE_OUTER_BOUND ( 'NONE', #12176, .T. ) ;
#9050=EDGE_LOOP ( 'NONE', ( #12789, #7033 ) ) ;
#9056=( BOUNDED_CURVE ( )  B_SPLINE_CURVE ( 3, ( #19753, #2152, #8461, #13207 ),
 .UNSPECIFIED., .F., .T. ) 
 B_SPLINE_CURVE_WITH_KNOTS ( ( 4, 4 ),
 ( 3.141592653589793116, 4.712388980384671910 ),
 .UNSPECIFIED. ) 
 CURVE ( )  GEOMETRIC_REPRESENTATION_ITEM ( )  RATIONAL_B_SPLINE_CURVE ( ( 1.000000000000000000, 0.8047378541243692673, 0.8047378541243692673, 1.000000000000000000 ) ) 
 REPRESENTATION_ITEM ( '' )  );
#9060=DIRECTION ( 'NONE',  ( 9.815121534730717399E-17, -1.000000000000000000, -0.000000000000000000 ) ) ;
#9066=DIRECTION ( 'NONE',  ( 4.784675105189226675E-17, 0.000000000000000000, 1.000000000000000000 ) ) ;
#9073=( LENGTH_UNIT ( ) NAMED_UNIT ( * ) SI_UNIT ( .MILLI., .METRE. ) );
#9080=ORIENTED_EDGE ( 'NONE', *, *, #5922, .F. ) ;
#9093=( NAMED_UNIT ( * ) PLANE_ANGLE_UNIT ( ) SI_UNIT ( $, .RADIAN. ) );
#9107=ORIENTED_EDGE ( 'NONE', *, *, #17846, .T. ) ;
#9113=ORIENTED_EDGE ( 'NONE', *, *, #11137, .F. ) ;
#9138=CARTESIAN_POINT ( 'NONE',  ( 53.48937290013658696, 122.8810204491430369, 280.0825295754780768 ) ) ;
#9158=( GEOMETRIC_REPRESENTATION_CONTEXT ( 3 ) GLOBAL_UNCERTAINTY_ASSIGNED_CONTEXT ( ( #8299 ) ) GLOBAL_UNIT_ASSIGNED_CONTEXT ( ( #6359, #259, #11283 ) ) REPRESENTATION_CONTEXT ( 'NONE', 'WORKASPACE' ) );
#9161=( NAMED_UNIT ( * ) SI_UNIT ( $, .STERADIAN. ) SOLID_ANGLE_UNIT ( ) );
#9194=DIRECTION ( 'NONE',  ( 1.000000000000000000, 0.000000000000000000, -0.000000000000000000 ) ) ;
#9219=AXIS2_PLACEMENT_3D ( 'NONE', #5655, #5554, #13592 ) ;
#9235=SURFACE_STYLE_USAGE ( .BOTH. , #10791 ) ;
#9258=FILL_AREA_STYLE_COLOUR ( '', #12879 ) ;
#9263=AXIS2_PLACEMENT_3D ( 'NONE', #13556, #9010, #13661 ) ;
#9289=EDGE_CURVE ( 'NONE', #7627, #9009, #10934, .T. ) ;
#9294=SURFACE_STYLE_USAGE ( .BOTH. , #7650 ) ;
#9296=( LENGTH_UNIT ( ) NAMED_UNIT ( * ) SI_UNIT ( .MILLI., .METRE. ) );
#9307=CARTESIAN_POINT ( 'NONE',  ( 53.48937290013659407, 49.66333933884487806, 252.0000000000000000 ) ) ;
#9327=SURFACE_STYLE_FILL_AREA ( #18701 ) ;
#9340=CARTESIAN_POINT ( 'NONE',  ( 111.4893729001366012, 127.7247684487574588, 254.0000000000000000 ) ) ;
#9341=STYLED_ITEM ( 'NONE', ( #4012 ), #12135 ) ;
#9345=EDGE_CURVE ( 'NONE', #1376, #18127, #189, .T. ) ;
#9349=PRODUCT_DEFINITION ( 'UNKNOWN', '', #14900, #7411 ) ;
#9391=FILL_AREA_STYLE ('',( #4648 ) ) ;
#9403=MECHANICAL_DESIGN_GEOMETRIC_PRESENTATION_REPRESENTATION('',(#11706),#7760);
#9405=VERTEX_POINT ( 'NONE', #15886 ) ;
#9412=FILL_AREA_STYLE ('',( #17241 ) ) ;
#9433=VERTEX_POINT ( 'NONE', #11438 ) ;
#9441=ORIENTED_EDGE ( 'NONE', *, *, #1476, .T. ) ;
#9478=AXIS2_PLACEMENT_3D ( 'NONE', #12534, #15956, #12853 ) ;
#9495=DIRECTION ( 'NONE',  ( 6.263247009234064878E-17, -0.6381222063396385646, 0.7699350945217602327 ) ) ;
#9497=CARTESIAN_POINT ( 'NONE',  ( 111.4893729001366154, 77.72476844875745883, 252.0000000000000000 ) ) ;
#9508=LINE ( 'NONE', #15814, #17598 ) ;
#9515=ORIENTED_EDGE ( 'NONE', *, *, #4148, .T. ) ;
#9516=VECTOR ( 'NONE', #7925, 1000.000000000000000 ) ;
#9524=DIRECTION ( 'NONE',  ( 1.000000000000000000, 9.815121534730718631E-17, 0.000000000000000000 ) ) ;
#9536=DIRECTION ( 'NONE',  ( -0.000000000000000000, -0.7791332379872890623, -0.6268583551835633649 ) ) ;
#9540=CYLINDRICAL_SURFACE ( 'NONE', #14478, 3.283624802691453848 ) ;
#9549=ORIENTED_EDGE ( 'NONE', *, *, #13393, .F. ) ;
#9551=( NAMED_UNIT ( * ) SI_UNIT ( $, .STERADIAN. ) SOLID_ANGLE_UNIT ( ) );
#9639=LINE ( 'NONE', #11188, #14931 ) ;
#9693=AXIS2_PLACEMENT_3D ( 'NONE', #8893, #15183, #13638 ) ;
#9714=( BOUNDED_CURVE ( )  B_SPLINE_CURVE ( 3, ( #3232, #17247, #10760, #13954 ),
 .UNSPECIFIED., .F., .T. ) 
 B_SPLINE_CURVE_WITH_KNOTS ( ( 4, 4 ),
 ( 4.712388980384689674, 6.283185307179586232 ),
 .UNSPECIFIED. ) 
 CURVE ( )  GEOMETRIC_REPRESENTATION_ITEM ( )  RATIONAL_B_SPLINE_CURVE ( ( 1.000000000000000000, 0.8047378541243649375, 0.8047378541243649375, 1.000000000000000000 ) ) 
 REPRESENTATION_ITEM ( '' )  );
#9753=CARTESIAN_POINT ( 'NONE',  ( 109.4893729001365870, 209.7811923590224978, 348.0151256184570343 ) ) ;
#9754=CARTESIAN_POINT ( 'NONE',  ( 111.4893729001366012, 211.0574367717017594, 346.4752554294135507 ) ) ;
#9776=( NAMED_UNIT ( * ) PLANE_ANGLE_UNIT ( ) SI_UNIT ( $, .RADIAN. ) );
#9780=PRESENTATION_STYLE_ASSIGNMENT (( #13285 ) ) ;
#9791=ORIENTED_EDGE ( 'NONE', *, *, #10396, .T. ) ;
#9794=CARTESIAN_POINT ( 'NONE',  ( 53.48937290013660117, 77.72476844875745883, 252.0000000000000000 ) ) ;
#9812=DIRECTION ( 'NONE',  ( -1.000000000000000000, -9.815121534730717399E-17, 0.000000000000000000 ) ) ;
#9813=EDGE_LOOP ( 'NONE', ( #2337, #5410, #16281, #2146 ) ) ;
#9871=SURFACE_SIDE_STYLE ('',( #75 ) ) ;
#9882=COLOUR_RGB ( '', 0.31764706, 0.68627451, 0.89019608) ;
#9905=SURFACE_STYLE_USAGE ( .BOTH. , #3724 ) ;
#9909=SURFACE_SIDE_STYLE ('',( #16326 ) ) ;
#9910=UNCERTAINTY_MEASURE_WITH_UNIT (LENGTH_MEASURE( 1.000000000000000082E-05 ), #7028, 'distance_accuracy_value', 'NONE');
#9913=ORIENTED_EDGE ( 'NONE', *, *, #13024, .F. ) ;
#9927=EDGE_CURVE ( 'NONE', #4060, #2417, #4495, .T. ) ;
#9957=AXIS2_PLACEMENT_3D ( 'NONE', #3377, #1822, #12455 ) ;
#9962=AXIS2_PLACEMENT_3D ( 'NONE', #3186, #15278, #3283 ) ;
#10001=DIRECTION ( 'NONE',  ( 0.000000000000000000, 1.000000000000000000, 0.000000000000000000 ) ) ;
#10005=FILL_AREA_STYLE_COLOUR ( '', #11679 ) ;
#10007=VECTOR ( 'NONE', #19310, 1000.000000000000227 ) ;
#10023=LINE ( 'NONE', #11977, #12708 ) ;
#10029=SURFACE_STYLE_USAGE ( .BOTH. , #17751 ) ;
#10054=STYLED_ITEM ( 'NONE', ( #3423 ), #1836 ) ;
#10062=( NAMED_UNIT ( * ) SI_UNIT ( $, .STERADIAN. ) SOLID_ANGLE_UNIT ( ) );
#10137=ORIENTED_EDGE ( 'NONE', *, *, #13156, .F. ) ;
#10145=( NAMED_UNIT ( * ) PLANE_ANGLE_UNIT ( ) SI_UNIT ( $, .RADIAN. ) );
#10148=CARTESIAN_POINT ( 'NONE',  ( 53.48937290013659407, 211.0574367717017594, 346.4752554294135507 ) ) ;
#10184=CIRCLE ( 'NONE', #17416, 3.283624802691453848 ) ;
#10196=CIRCLE ( 'NONE', #4278, 2.000000000000001776 ) ;
#10213=EDGE_CURVE ( 'NONE', #10931, #15732, #11698, .T. ) ;
#10286=( GEOMETRIC_REPRESENTATION_CONTEXT ( 3 ) GLOBAL_UNCERTAINTY_ASSIGNED_CONTEXT ( ( #292 ) ) GLOBAL_UNIT_ASSIGNED_CONTEXT ( ( #17456, #1572, #11180 ) ) REPRESENTATION_CONTEXT ( 'NONE', 'WORKASPACE' ) );
#10307=( GEOMETRIC_REPRESENTATION_CONTEXT ( 3 ) GLOBAL_UNCERTAINTY_ASSIGNED_CONTEXT ( ( #12000 ) ) GLOBAL_UNIT_ASSIGNED_CONTEXT ( ( #8048, #209, #1623 ) ) REPRESENTATION_CONTEXT ( 'NONE', 'WORKASPACE' ) );
#10319=LINE ( 'NONE', #7041, #668 ) ;
#10329=( LENGTH_UNIT ( ) NAMED_UNIT ( * ) SI_UNIT ( .MILLI., .METRE. ) );
#10337=VERTEX_POINT ( 'NONE', #5908 ) ;
#10339=EDGE_CURVE ( 'NONE', #2573, #3307, #12185, .T. ) ;
#10346=ORIENTED_EDGE ( 'NONE', *, *, #2082, .T. ) ;
#10347=DIRECTION ( 'NONE',  ( 1.000000000000000000, 9.815121534730717399E-17, 0.000000000000000000 ) ) ;
#10367=DIRECTION ( 'NONE',  ( 0.000000000000000000, 1.000000000000000000, 0.000000000000000000 ) ) ;
#10381=CARTESIAN_POINT ( 'NONE',  ( 111.4893729001366012, 127.7247684487574588, 357.7985149490353933 ) ) ;
#10396=EDGE_CURVE ( 'NONE', #2161, #18128, #18567, .T. ) ;
#10404=ADVANCED_FACE ( 'NONE', ( #1753 ), #17337, .T. ) ;
#10405=LINE ( 'NONE', #13499, #4732 ) ;
#10409=DIRECTION ( 'NONE',  ( -1.000000000000000000, -3.816214432251725906E-17, 4.784675105189226675E-17 ) ) ;
#10415=CARTESIAN_POINT ( 'NONE',  ( 53.48937290013660828, 127.7247684487574020, 357.7985149490353933 ) ) ;
#10450=CARTESIAN_POINT ( 'NONE',  ( 53.48937290013659407, 129.7247684487574588, 283.6050404526570219 ) ) ;
#10459=VERTEX_POINT ( 'NONE', #9497 ) ;
#10497=CARTESIAN_POINT ( 'NONE',  ( 111.4893729001366012, 129.7247684487574588, 281.6050404526570219 ) ) ;
#10522=( GEOMETRIC_REPRESENTATION_CONTEXT ( 3 ) GLOBAL_UNCERTAINTY_ASSIGNED_CONTEXT ( ( #16514 ) ) GLOBAL_UNIT_ASSIGNED_CONTEXT ( ( #11193, #3264, #6468 ) ) REPRESENTATION_CONTEXT ( 'NONE', 'WORKASPACE' ) );
#10537=CIRCLE ( 'NONE', #5283, 2.000000000000001776 ) ;
#10569=CARTESIAN_POINT ( 'NONE',  ( 55.98937290013660117, 144.5787140289007198, 293.4524157190248275 ) ) ;
#10573=CARTESIAN_POINT ( 'NONE',  ( 109.4893729001366012, 127.7247684487574588, 368.0000000000000000 ) ) ;
#10598=FILL_AREA_STYLE ('',( #19862 ) ) ;
#10599=MECHANICAL_DESIGN_GEOMETRIC_PRESENTATION_REPRESENTATION('',(#6344),#4352);
#10641=CARTESIAN_POINT ( 'NONE',  ( 108.9893729001365870, 108.8727366810872468, 338.2196854716659118 ) ) ;
#10678=PRESENTATION_STYLE_ASSIGNMENT (( #4812 ) ) ;
#10704=FACE_OUTER_BOUND ( 'NONE', #14078, .T. ) ;
#10711=LINE ( 'NONE', #12069, #18667 ) ;
#10722=DIRECTION ( 'NONE',  ( 0.000000000000000000, 1.000000000000000000, 0.000000000000000000 ) ) ;
#10756=ORIENTED_EDGE ( 'NONE', *, *, #11655, .T. ) ;
#10760=CARTESIAN_POINT ( 'NONE',  ( 54.31780002488278569, 211.0574367717017594, 346.4752554294134939 ) ) ;
#10774=ADVANCED_FACE ( 'NONE', ( #14196, #12982 ), #18933, .T. ) ;
#10782=( LENGTH_UNIT ( ) NAMED_UNIT ( * ) SI_UNIT ( .MILLI., .METRE. ) );
#10786=CARTESIAN_POINT ( 'NONE',  ( 108.9893729001366154, 130.3113892758444194, 284.0770112900635809 ) ) ;
#10790=LINE ( 'NONE', #465, #7306 ) ;
#10791=SURFACE_SIDE_STYLE ('',( #4512 ) ) ;
#10796=VERTEX_POINT ( 'NONE', #5241 ) ;
#10827=ORIENTED_EDGE ( 'NONE', *, *, #8661, .T. ) ;
#10828=EDGE_CURVE ( 'NONE', #19038, #8344, #6991, .T. ) ;
#10853=( NAMED_UNIT ( * ) PLANE_ANGLE_UNIT ( ) SI_UNIT ( $, .RADIAN. ) );
#10893=ORIENTED_EDGE ( 'NONE', *, *, #7353, .T. ) ;
#10915=DIRECTION ( 'NONE',  ( 9.815121534730717399E-17, -1.000000000000000000, 0.000000000000000000 ) ) ;
#10931=VERTEX_POINT ( 'NONE', #3472 ) ;
#10934=LINE ( 'NONE', #6201, #18625 ) ;
#10958=PLANE ( 'NONE',  #18266 ) ;
#10967=ORIENTED_EDGE ( 'NONE', *, *, #11137, .T. ) ;
#10972=CIRCLE ( 'NONE', #8018, 2.000000000000001776 ) ;
#10975=ORIENTED_EDGE ( 'NONE', *, *, #1395, .F. ) ;
#10985=CARTESIAN_POINT ( 'NONE',  ( 53.48937290013658696, 122.8810204491430369, 280.0825295754780768 ) ) ;
#10995=PRESENTATION_STYLE_ASSIGNMENT (( #9235 ) ) ;
#11001=EDGE_CURVE ( 'NONE', #258, #18079, #3770, .T. ) ;
#11027=ORIENTED_EDGE ( 'NONE', *, *, #407, .T. ) ;
#11054=CIRCLE ( 'NONE', #12697, 2.000000000000001776 ) ;
#11059=FILL_AREA_STYLE_COLOUR ( '', #1777 ) ;
#11089=DIRECTION ( 'NONE',  ( 1.000000000000000000, 9.815121534730718631E-17, -0.000000000000000000 ) ) ;
#11096=( NAMED_UNIT ( * ) PLANE_ANGLE_UNIT ( ) SI_UNIT ( $, .RADIAN. ) );
#11099=AXIS2_PLACEMENT_3D ( 'NONE', #8358, #4958, #11230 ) ;
#11101=CARTESIAN_POINT ( 'NONE',  ( 111.4893729001366012, 125.7247684487574588, 252.0000000000000000 ) ) ;
#11124=ORIENTED_EDGE ( 'NONE', *, *, #2921, .F. ) ;
#11137=EDGE_CURVE ( 'NONE', #1376, #16358, #12008, .T. ) ;
#11142=EDGE_CURVE ( 'NONE', #9433, #2901, #4184, .T. ) ;
#11157=DIRECTION ( 'NONE',  ( -1.000000000000000000, -1.047380211910524510E-15, -2.094760423821049019E-15 ) ) ;
#11180=( NAMED_UNIT ( * ) SI_UNIT ( $, .STERADIAN. ) SOLID_ANGLE_UNIT ( ) );
#11188=CARTESIAN_POINT ( 'NONE',  ( 55.98937290013660828, 143.7407018517681365, 294.8816803532601512 ) ) ;
#11193=( LENGTH_UNIT ( ) NAMED_UNIT ( * ) SI_UNIT ( .MILLI., .METRE. ) );
#11204=PRESENTATION_STYLE_ASSIGNMENT (( #3064 ) ) ;
#11208=STYLED_ITEM ( 'NONE', ( #1197 ), #17155 ) ;
#11215=FILL_AREA_STYLE ('',( #6702 ) ) ;
#11230=DIRECTION ( 'NONE',  ( 0.000000000000000000, -0.6235460666509320404, 0.7817866094812263578 ) ) ;
#11276=FILL_AREA_STYLE ('',( #17769 ) ) ;
#11283=( NAMED_UNIT ( * ) SI_UNIT ( $, .STERADIAN. ) SOLID_ANGLE_UNIT ( ) );
#11293=DIRECTION ( 'NONE',  ( 6.263247009234063646E-17, -0.6381222063396385646, 0.7699350945217602327 ) ) ;
#11314=FILL_AREA_STYLE_COLOUR ( '', #1805 ) ;
#11320=( GEOMETRIC_REPRESENTATION_CONTEXT ( 3 ) GLOBAL_UNCERTAINTY_ASSIGNED_CONTEXT ( ( #4178 ) ) GLOBAL_UNIT_ASSIGNED_CONTEXT ( ( #19450, #18014, #7015 ) ) REPRESENTATION_CONTEXT ( 'NONE', 'WORKASPACE' ) );
#11346=AXIS2_PLACEMENT_3D ( 'NONE', #17045, #15813, #4477 ) ;
#11352=FILL_AREA_STYLE_COLOUR ( '', #5778 ) ;
#11355=CARTESIAN_POINT ( 'NONE',  ( 111.4893729001366012, 129.7247684487574588, 370.0000000000000000 ) ) ;
#11369=MECHANICAL_DESIGN_GEOMETRIC_PRESENTATION_REPRESENTATION('',(#5450),#6792);
#11384=EDGE_LOOP ( 'NONE', ( #6475, #10827 ) ) ;
#11403=VECTOR ( 'NONE', #16711, 1000.000000000000000 ) ;
#11410=ORIENTED_EDGE ( 'NONE', *, *, #19943, .T. ) ;
#11438=CARTESIAN_POINT ( 'NONE',  ( 53.48937290013659407, 129.7247684487574588, 283.6050404526570219 ) ) ;
#11440=ADVANCED_FACE ( 'NONE', ( #17848 ), #19386, .T. ) ;
#11453=ORIENTED_EDGE ( 'NONE', *, *, #9289, .F. ) ;
#11459=ORIENTED_EDGE ( 'NONE', *, *, #17227, .T. ) ;
#11477=ORIENTED_EDGE ( 'NONE', *, *, #11793, .T. ) ;
#11478=ORIENTED_EDGE ( 'NONE', *, *, #7490, .T. ) ;
#11481=ORIENTED_EDGE ( 'NONE', *, *, #1098, .F. ) ;
#11487=CARTESIAN_POINT ( 'NONE',  ( 111.4893729001366012, 125.7247684487574588, 254.0000000000000000 ) ) ;
#11491=CARTESIAN_POINT ( 'NONE',  ( 53.48937290013659407, 127.7247684487574588, 254.0000000000000000 ) ) ;
#11500=DIRECTION ( 'NONE',  ( 0.000000000000000000, 1.000000000000000000, 0.000000000000000000 ) ) ;
#11513=( NAMED_UNIT ( * ) SI_UNIT ( $, .STERADIAN. ) SOLID_ANGLE_UNIT ( ) );
#11516=DIRECTION ( 'NONE',  ( 1.000000000000000000, 9.815121534730718631E-17, -0.000000000000000000 ) ) ;
#11537=PRESENTATION_STYLE_ASSIGNMENT (( #5464 ) ) ;
#11550=EDGE_CURVE ( 'NONE', #18127, #9405, #5686, .T. ) ;
#11585=DIRECTION ( 'NONE',  ( 1.632406474348796386E-15, -0.7791332379872890623, -0.6268583551835632539 ) ) ;
#11601=PLANE ( 'NONE',  #9263 ) ;
#11619=DIRECTION ( 'NONE',  ( 0.000000000000000000, -2.352167425053297897E-16, -1.000000000000000000 ) ) ;
#11655=EDGE_CURVE ( 'NONE', #323, #6446, #3106, .T. ) ;
#11658=ORIENTED_EDGE ( 'NONE', *, *, #2351, .F. ) ;
#11663=ORIENTED_EDGE ( 'NONE', *, *, #15060, .F. ) ;
#11669=MECHANICAL_DESIGN_GEOMETRIC_PRESENTATION_REPRESENTATION('',(#15645),#4761);
#11675=VECTOR ( 'NONE', #14642, 1000.000000000000000 ) ;
#11679=COLOUR_RGB ( '', 0.40784314, 0.44705882, 0.49803922) ;
#11688=VECTOR ( 'NONE', #8833, 1000.000000000000114 ) ;
#11698=LINE ( 'NONE', #3954, #10007 ) ;
#11706=STYLED_ITEM ( 'NONE', ( #14905 ), #8765 ) ;
#11711=LINE ( 'NONE', #2299, #2480 ) ;
#11721=ORIENTED_EDGE ( 'NONE', *, *, #1611, .T. ) ;
#11738=LINE ( 'NONE', #19343, #2371 ) ;
#11740=EDGE_LOOP ( 'NONE', ( #752, #12165, #11124, #11481 ) ) ;
#11756=DIRECTION ( 'NONE',  ( 1.000000000000000000, 1.314570224013242627E-15, 9.702050138162214733E-16 ) ) ;
#11762=FILL_AREA_STYLE ('',( #10005 ) ) ;
#11764=EDGE_CURVE ( 'NONE', #8530, #16423, #14173, .T. ) ;
#11793=EDGE_CURVE ( 'NONE', #2161, #12975, #7026, .T. ) ;
#11794=VERTEX_POINT ( 'NONE', #405 ) ;
#11803=COLOUR_RGB ( '', 0.09019608, 0.27058824, 0.51372549) ;
#11817=ORIENTED_EDGE ( 'NONE', *, *, #710, .F. ) ;
#11827=( BOUNDED_CURVE ( )  B_SPLINE_CURVE ( 3, ( #13079, #17683, #8112, #9753 ),
 .UNSPECIFIED., .F., .T. ) 
 B_SPLINE_CURVE_WITH_KNOTS ( ( 4, 4 ),
 ( 1.570796326794896558, 3.141592653589793116 ),
 .UNSPECIFIED. ) 
 CURVE ( )  GEOMETRIC_REPRESENTATION_ITEM ( )  RATIONAL_B_SPLINE_CURVE ( ( 1.000000000000000000, 0.8047378541243649375, 0.8047378541243649375, 1.000000000000000000 ) ) 
 REPRESENTATION_ITEM ( '' )  );
#11830=MECHANICAL_DESIGN_GEOMETRIC_PRESENTATION_REPRESENTATION('',(#13784),#3261);
#11836=SURFACE_SIDE_STYLE ('',( #18200 ) ) ;
#11855=CARTESIAN_POINT ( 'NONE',  ( 111.4893729001366012, 126.1646452518344859, 280.0825295754780768 ) ) ;
#11857=STYLED_ITEM ( 'NONE', ( #10995 ), #16397 ) ;
#11885=SURFACE_SIDE_STYLE ('',( #1126 ) ) ;
#11890=PRESENTATION_STYLE_ASSIGNMENT (( #1007 ) ) ;
#11892=ORIENTED_EDGE ( 'NONE', *, *, #8661, .F. ) ;
#11925=LINE ( 'NONE', #4096, #8887 ) ;
#11935=PRESENTATION_STYLE_ASSIGNMENT (( #5645 ) ) ;
#11946=EDGE_CURVE ( 'NONE', #889, #6644, #11827, .T. ) ;
#11950=SURFACE_STYLE_USAGE ( .BOTH. , #16605 ) ;
#11962=SURFACE_STYLE_USAGE ( .BOTH. , #13509 ) ;
#11973=UNCERTAINTY_MEASURE_WITH_UNIT (LENGTH_MEASURE( 1.000000000000000082E-05 ), #12051, 'distance_accuracy_value', 'NONE');
#11976=CARTESIAN_POINT ( 'NONE',  ( 111.4893729001366012, 119.5973956464515879, 322.0399576098686225 ) ) ;
#11977=CARTESIAN_POINT ( 'NONE',  ( 109.4893729001366012, 127.7247684487574588, 370.0000000000000000 ) ) ;
#11991=ORIENTED_EDGE ( 'NONE', *, *, #19640, .F. ) ;
#12000=UNCERTAINTY_MEASURE_WITH_UNIT (LENGTH_MEASURE( 1.000000000000000082E-05 ), #8048, 'distance_accuracy_value', 'NONE');
#12007=DIRECTION ( 'NONE',  ( 0.000000000000000000, 0.000000000000000000, 1.000000000000000000 ) ) ;
#12008=LINE ( 'NONE', #6134, #18677 ) ;
#12035=STYLED_ITEM ( 'NONE', ( #3592 ), #10774 ) ;
#12047=SURFACE_STYLE_USAGE ( .BOTH. , #11836 ) ;
#12051=( LENGTH_UNIT ( ) NAMED_UNIT ( * ) SI_UNIT ( .MILLI., .METRE. ) );
#12053=ORIENTED_EDGE ( 'NONE', *, *, #10213, .F. ) ;
#12065=CARTESIAN_POINT ( 'NONE',  ( 55.48937290013659407, 209.7811923590224978, 348.0151256184570343 ) ) ;
#12069=CARTESIAN_POINT ( 'NONE',  ( 53.48937290013659407, 129.7247684487574588, 281.6050404526570219 ) ) ;
#12074=VERTEX_POINT ( 'NONE', #10497 ) ;
#12075=ADVANCED_FACE ( 'NONE', ( #4319 ), #1191, .F. ) ;
#12122=CARTESIAN_POINT ( 'NONE',  ( 53.48937290013659407, 209.7811923590224978, 348.0151256184570343 ) ) ;
#12135=ADVANCED_FACE ( 'NONE', ( #12149 ), #12245, .T. ) ;
#12138=ORIENTED_EDGE ( 'NONE', *, *, #6579, .F. ) ;
#12149=FACE_OUTER_BOUND ( 'NONE', #17255, .T. ) ;
#12154=PLANE ( 'NONE',  #42 ) ;
#12165=ORIENTED_EDGE ( 'NONE', *, *, #14371, .T. ) ;
#12176=EDGE_LOOP ( 'NONE', ( #14499, #20291, #3339, #11027 ) ) ;
#12185=LINE ( 'NONE', #10641, #13334 ) ;
#12187=ORIENTED_EDGE ( 'NONE', *, *, #11550, .F. ) ;
#12206=VECTOR ( 'NONE', #15775, 1000.000000000000000 ) ;
#12212=( NAMED_UNIT ( * ) SI_UNIT ( $, .STERADIAN. ) SOLID_ANGLE_UNIT ( ) );
#12220=STYLED_ITEM ( 'NONE', ( #13259 ), #17761 ) ;
#12226=AXIS2_PLACEMENT_3D ( 'NONE', #13267, #671, #14598 ) ;
#12231=EDGE_LOOP ( 'NONE', ( #15240, #20346, #8933, #19397 ) ) ;
#12239=STYLED_ITEM ( 'NONE', ( #6800 ), #8166 ) ;
#12245=PLANE ( 'NONE',  #6402 ) ;
#12254=ORIENTED_EDGE ( 'NONE', *, *, #6628, .T. ) ;
#12262=ORIENTED_EDGE ( 'NONE', *, *, #19885, .T. ) ;
#12273=CARTESIAN_POINT ( 'NONE',  ( 111.4893729001366012, 129.7247684487574588, 370.0000000000000000 ) ) ;
#12291=( NAMED_UNIT ( * ) PLANE_ANGLE_UNIT ( ) SI_UNIT ( $, .RADIAN. ) );
#12303=COLOUR_RGB ( '', 0.40784314, 0.44705882, 0.49803922) ;
#12329=CYLINDRICAL_SURFACE ( 'NONE', #13002, 3.283624802691453848 ) ;
#12363=( NAMED_UNIT ( * ) PLANE_ANGLE_UNIT ( ) SI_UNIT ( $, .RADIAN. ) );
#12383=CARTESIAN_POINT ( 'NONE',  ( 53.48937290013658696, 119.5973956464515879, 322.0399576098686225 ) ) ;
#12402=( NAMED_UNIT ( * ) PLANE_ANGLE_UNIT ( ) SI_UNIT ( $, .RADIAN. ) );
#12408=PLANE ( 'NONE',  #1813 ) ;
#12413=EDGE_CURVE ( 'NONE', #7981, #6644, #13680, .T. ) ;
#12414=DIRECTION ( 'NONE',  ( -1.000000000000000000, -9.815121534730717399E-17, 0.000000000000000000 ) ) ;
#12423=ADVANCED_FACE ( 'NONE', ( #15333 ), #19631, .F. ) ;
#12431=CARTESIAN_POINT ( 'NONE',  ( -77.99033078109007988, 127.7247684487574304, 254.0000000000000000 ) ) ;
#12455=DIRECTION ( 'NONE',  ( 0.000000000000000000, 1.000000000000000000, 0.000000000000000000 ) ) ;
#12460=MECHANICAL_DESIGN_GEOMETRIC_PRESENTATION_REPRESENTATION('',(#6884),#9158);
#12465=ADVANCED_FACE ( 'NONE', ( #17272 ), #12329, .F. ) ;
#12479=PLANE ( 'NONE',  #12965 ) ;
#12504=FILL_AREA_STYLE ('',( #6533 ) ) ;
#12519=EDGE_CURVE ( 'NONE', #12769, #7627, #14172, .T. ) ;
#12532=SURFACE_SIDE_STYLE ('',( #4502 ) ) ;
#12534=CARTESIAN_POINT ( 'NONE',  ( -77.99033078109007988, 127.7247684487574304, 357.7985149490353933 ) ) ;
#12539=CARTESIAN_POINT ( 'NONE',  ( 108.9893729001365870, 144.5787140289007766, 293.4524157190248275 ) ) ;
#12540=FILL_AREA_STYLE_COLOUR ( '', #6927 ) ;
#12567=ORIENTED_EDGE ( 'NONE', *, *, #17846, .F. ) ;
#12615=DIRECTION ( 'NONE',  ( 1.387778780781446415E-16, -1.000000000000000000, 0.000000000000000000 ) ) ;
#12664=FILL_AREA_STYLE_COLOUR ( '', #18817 ) ;
#12688=CARTESIAN_POINT ( 'NONE',  ( 53.48937290013659407, 127.7247684487574304, 252.0000000000000000 ) ) ;
#12694=CARTESIAN_POINT ( 'NONE',  ( 109.4893729001365870, 209.7811923590224978, 348.0151256184570343 ) ) ;
#12697=AXIS2_PLACEMENT_3D ( 'NONE', #20018, #4087, #10367 ) ;
#12708=VECTOR ( 'NONE', #2262, 1000.000000000000000 ) ;
#12715=DIRECTION ( 'NONE',  ( -6.263247009234064878E-17, 0.6381222063396385646, -0.7699350945217602327 ) ) ;
#12763=EDGE_LOOP ( 'NONE', ( #19796, #5485, #20285, #11817 ) ) ;
#12769=VERTEX_POINT ( 'NONE', #19611 ) ;
#12772=SURFACE_SIDE_STYLE ('',( #3180 ) ) ;
#12773=DIRECTION ( 'NONE',  ( 0.000000000000000000, 0.7817866094812263578, 0.6235460666509320404 ) ) ;
#12784=ORIENTED_EDGE ( 'NONE', *, *, #14289, .T. ) ;
#12789=ORIENTED_EDGE ( 'NONE', *, *, #13174, .F. ) ;
#12798=PLANE ( 'NONE',  #11099 ) ;
#12804=EDGE_CURVE ( 'NONE', #1294, #4349, #6136, .T. ) ;
#12831=VERTEX_POINT ( 'NONE', #7665 ) ;
#12853=DIRECTION ( 'NONE',  ( -1.000000000000000000, -9.815121534730718631E-17, 0.000000000000000000 ) ) ;
#12879=COLOUR_RGB ( '', 0.09019608, 0.27058824, 0.51372549) ;
#12890=UNCERTAINTY_MEASURE_WITH_UNIT (LENGTH_MEASURE( 1.000000000000000082E-05 ), #19405, 'distance_accuracy_value', 'NONE');
#12952=ORIENTED_EDGE ( 'NONE', *, *, #7152, .F. ) ;
#12965=AXIS2_PLACEMENT_3D ( 'NONE', #13011, #11756, #16499 ) ;
#12975=VERTEX_POINT ( 'NONE', #6853 ) ;
#12982=FACE_OUTER_BOUND ( 'NONE', #15452, .T. ) ;
#12989=MECHANICAL_DESIGN_GEOMETRIC_PRESENTATION_REPRESENTATION('',(#5730),#13272);
#13000=ORIENTED_EDGE ( 'NONE', *, *, #8834, .T. ) ;
#13002=AXIS2_PLACEMENT_3D ( 'NONE', #10985, #11089, #14076 ) ;
#13011=CARTESIAN_POINT ( 'NONE',  ( 108.9893729001365870, 108.8727366810872468, 338.2196854716659118 ) ) ;
#13024=EDGE_CURVE ( 'NONE', #15732, #4060, #9508, .T. ) ;
#13032=UNCERTAINTY_MEASURE_WITH_UNIT (LENGTH_MEASURE( 1.000000000000000082E-05 ), #3743, 'distance_accuracy_value', 'NONE');
#13079=CARTESIAN_POINT ( 'NONE',  ( 111.4893729001366012, 208.2227610943810134, 346.7612763259490407 ) ) ;
#13156=EDGE_CURVE ( 'NONE', #7981, #323, #13924, .T. ) ;
#13167=FACE_OUTER_BOUND ( 'NONE', #12231, .T. ) ;
#13174=EDGE_CURVE ( 'NONE', #14376, #12975, #8634, .T. ) ;
#13181=FILL_AREA_STYLE ('',( #6894 ) ) ;
#13182=DIRECTION ( 'NONE',  ( 0.000000000000000000, 0.000000000000000000, 1.000000000000000000 ) ) ;
#13189=SURFACE_STYLE_FILL_AREA ( #16188 ) ;
#13207=CARTESIAN_POINT ( 'NONE',  ( 111.4893729001366012, 209.4935875941501422, 345.2279431939882670 ) ) ;
#13212=AXIS2_PLACEMENT_3D ( 'NONE', #17929, #3621, #10001 ) ;
#13214=DIRECTION ( 'NONE',  ( 7.897989220727750531E-17, -0.8046756418431283420, 0.5937146717273790175 ) ) ;
#13229=MECHANICAL_DESIGN_GEOMETRIC_PRESENTATION_REPRESENTATION('',(#7956),#14535);
#13230=( NAMED_UNIT ( * ) SI_UNIT ( $, .STERADIAN. ) SOLID_ANGLE_UNIT ( ) );
#13232=LINE ( 'NONE', #8388, #17785 ) ;
#13259=PRESENTATION_STYLE_ASSIGNMENT (( #14789 ) ) ;
#13267=CARTESIAN_POINT ( 'NONE',  ( 53.48937290013658696, 122.8810204491430369, 322.0399576098686225 ) ) ;
#13272=( GEOMETRIC_REPRESENTATION_CONTEXT ( 3 ) GLOBAL_UNCERTAINTY_ASSIGNED_CONTEXT ( ( #5812 ) ) GLOBAL_UNIT_ASSIGNED_CONTEXT ( ( #4128, #3177, #14299 ) ) REPRESENTATION_CONTEXT ( 'NONE', 'WORKASPACE' ) );
#13285=SURFACE_STYLE_USAGE ( .BOTH. , #3598 ) ;
#13302=PLANE ( 'NONE',  #8374 ) ;
#13321=( GEOMETRIC_REPRESENTATION_CONTEXT ( 3 ) GLOBAL_UNCERTAINTY_ASSIGNED_CONTEXT ( ( #3929 ) ) GLOBAL_UNIT_ASSIGNED_CONTEXT ( ( #10782, #1481, #20139 ) ) REPRESENTATION_CONTEXT ( 'NONE', 'WORKASPACE' ) );
#13334=VECTOR ( 'NONE', #4058, 1000.000000000000227 ) ;
#13358=VECTOR ( 'NONE', #5558, 1000.000000000000000 ) ;
#13372=ORIENTED_EDGE ( 'NONE', *, *, #2812, .F. ) ;
#13389=( NAMED_UNIT ( * ) SI_UNIT ( $, .STERADIAN. ) SOLID_ANGLE_UNIT ( ) );
#13393=EDGE_CURVE ( 'NONE', #4349, #8344, #11738, .T. ) ;
#13402=ORIENTED_EDGE ( 'NONE', *, *, #12804, .F. ) ;
#13408=VECTOR ( 'NONE', #7386, 1000.000000000000000 ) ;
#13422=ORIENTED_EDGE ( 'NONE', *, *, #20093, .T. ) ;
#13464=SHAPE_DEFINITION_REPRESENTATION ( #7782, #4054 ) ;
#13474=FACE_OUTER_BOUND ( 'NONE', #223, .T. ) ;
#13478=FILL_AREA_STYLE ('',( #2219 ) ) ;
#13481=FILL_AREA_STYLE ('',( #1167 ) ) ;
#13494=AXIS2_PLACEMENT_3D ( 'NONE', #8495, #10347, #16658 ) ;
#13499=CARTESIAN_POINT ( 'NONE',  ( 111.4893729001366012, 127.7247684487574304, 368.0000000000000000 ) ) ;
#13509=SURFACE_SIDE_STYLE ('',( #18644 ) ) ;
#13512=ORIENTED_EDGE ( 'NONE', *, *, #16906, .T. ) ;
#13518=ADVANCED_FACE ( 'NONE', ( #7200 ), #2541, .T. ) ;
#13556=CARTESIAN_POINT ( 'NONE',  ( 111.4893729001366154, 77.72476844875745883, 250.0000000000000000 ) ) ;
#13568=DIRECTION ( 'NONE',  ( 1.387778780781446415E-16, -1.000000000000000000, 0.000000000000000000 ) ) ;
#13592=DIRECTION ( 'NONE',  ( 0.000000000000000000, 1.000000000000000000, 0.000000000000000000 ) ) ;
#13638=DIRECTION ( 'NONE',  ( 0.000000000000000000, 1.000000000000000000, 0.000000000000000000 ) ) ;
#13661=DIRECTION ( 'NONE',  ( 1.000000000000000000, 9.815121534730717399E-17, 0.000000000000000000 ) ) ;
#13680=LINE ( 'NONE', #12122, #4767 ) ;
#13685=( LENGTH_UNIT ( ) NAMED_UNIT ( * ) SI_UNIT ( .MILLI., .METRE. ) );
#13711=MECHANICAL_DESIGN_GEOMETRIC_PRESENTATION_REPRESENTATION('',(#19804),#18957);
#13728=LINE ( 'NONE', #12273, #3813 ) ;
#13755=EDGE_LOOP ( 'NONE', ( #19141, #19439, #1542, #19465, #17078, #9515 ) ) ;
#13784=STYLED_ITEM ( 'NONE', ( #5587 ), #5113 ) ;
#13799=VECTOR ( 'NONE', #20274, 1000.000000000000000 ) ;
#13815=VECTOR ( 'NONE', #14806, 1000.000000000000000 ) ;
#13872=LINE ( 'NONE', #10786, #6701 ) ;
#13903=ORIENTED_EDGE ( 'NONE', *, *, #9345, .F. ) ;
#13910=ORIENTED_EDGE ( 'NONE', *, *, #3173, .F. ) ;
#13924=( BOUNDED_CURVE ( )  B_SPLINE_CURVE ( 3, ( #20281, #7824, #193, #1716 ),
 .UNSPECIFIED., .F., .T. ) 
 B_SPLINE_CURVE_WITH_KNOTS ( ( 4, 4 ),
 ( 0.000000000000000000, 1.570796326794907438 ),
 .UNSPECIFIED. ) 
 CURVE ( )  GEOMETRIC_REPRESENTATION_ITEM ( )  RATIONAL_B_SPLINE_CURVE ( ( 1.000000000000000000, 0.8047378541243623840, 0.8047378541243623840, 1.000000000000000000 ) ) 
 REPRESENTATION_ITEM ( '' )  );
#13934=ORIENTED_EDGE ( 'NONE', *, *, #15060, .T. ) ;
#13935=( LENGTH_UNIT ( ) NAMED_UNIT ( * ) SI_UNIT ( .MILLI., .METRE. ) );
#13943=CARTESIAN_POINT ( 'NONE',  ( 109.4893729001366012, 129.7247684487574588, 368.0000000000000000 ) ) ;
#13949=CARTESIAN_POINT ( 'NONE',  ( 53.48937290013660117, 77.72476844875745883, 250.0000000000000000 ) ) ;
#13954=CARTESIAN_POINT ( 'NONE',  ( 55.48937290013659407, 211.0574367717017594, 346.4752554294135507 ) ) ;
#13961=LINE ( 'NONE', #7784, #2023 ) ;
#13983=COLOUR_RGB ( '', 0.66274510, 0.83137255, 0.94901961) ;
#13991=( NAMED_UNIT ( * ) SI_UNIT ( $, .STERADIAN. ) SOLID_ANGLE_UNIT ( ) );
#14003=SURFACE_SIDE_STYLE ('',( #4926 ) ) ;
#14069=ORIENTED_EDGE ( 'NONE', *, *, #6833, .F. ) ;
#14076=DIRECTION ( 'NONE',  ( 0.000000000000000000, 1.000000000000000000, 0.000000000000000000 ) ) ;
#14078=EDGE_LOOP ( 'NONE', ( #11892, #1179, #8726, #3431 ) ) ;
#14079=FILL_AREA_STYLE ('',( #1483 ) ) ;
#14094=CARTESIAN_POINT ( 'NONE',  ( 111.4893729001366012, 127.7247684487574588, 370.0000000000000000 ) ) ;
#14110=ORIENTED_EDGE ( 'NONE', *, *, #10828, .F. ) ;
#14117=SURFACE_SIDE_STYLE ('',( #1526 ) ) ;
#14172=LINE ( 'NONE', #11491, #6750 ) ;
#14173=CIRCLE ( 'NONE', #13212, 2.000000000000001776 ) ;
#14181=DIRECTION ( 'NONE',  ( -7.557006526585458208E-17, 0.7699350945217602327, 0.6381222063396385646 ) ) ;
#14182=SURFACE_STYLE_FILL_AREA ( #4915 ) ;
#14183=ORIENTED_EDGE ( 'NONE', *, *, #6780, .F. ) ;
#14195=FILL_AREA_STYLE_COLOUR ( '', #19463 ) ;
#14196=FACE_BOUND ( 'NONE', #3924, .T. ) ;
#14212=CIRCLE ( 'NONE', #12226, 3.283624802691453848 ) ;
#14215=ORIENTED_EDGE ( 'NONE', *, *, #17549, .T. ) ;
#14222=PRESENTATION_STYLE_ASSIGNMENT (( #1850 ) ) ;
#14224=AXIS2_PLACEMENT_3D ( 'NONE', #20239, #18886, #3237 ) ;
#14238=MECHANICAL_DESIGN_GEOMETRIC_PRESENTATION_REPRESENTATION('',(#8974),#3036);
#14284=FACE_OUTER_BOUND ( 'NONE', #442, .T. ) ;
#14289=EDGE_CURVE ( 'NONE', #16423, #19149, #17157, .T. ) ;
#14299=( NAMED_UNIT ( * ) SI_UNIT ( $, .STERADIAN. ) SOLID_ANGLE_UNIT ( ) );
#14304=FACE_OUTER_BOUND ( 'NONE', #20313, .T. ) ;
#14305=( NAMED_UNIT ( * ) SI_UNIT ( $, .STERADIAN. ) SOLID_ANGLE_UNIT ( ) );
#14321=( GEOMETRIC_REPRESENTATION_CONTEXT ( 3 ) GLOBAL_UNCERTAINTY_ASSIGNED_CONTEXT ( ( #16327 ) ) GLOBAL_UNIT_ASSIGNED_CONTEXT ( ( #17609, #16089, #14506 ) ) REPRESENTATION_CONTEXT ( 'NONE', 'WORKASPACE' ) );
#14339=DIRECTION ( 'NONE',  ( -6.263247009234064878E-17, 0.6381222063396385646, -0.7699350945217602327 ) ) ;
#14369=ORIENTED_EDGE ( 'NONE', *, *, #16196, .T. ) ;
#14371=EDGE_CURVE ( 'NONE', #16025, #19038, #19650, .T. ) ;
#14376=VERTEX_POINT ( 'NONE', #11855 ) ;
#14380=( NAMED_UNIT ( * ) SI_UNIT ( $, .STERADIAN. ) SOLID_ANGLE_UNIT ( ) );
#14389=( NAMED_UNIT ( * ) SI_UNIT ( $, .STERADIAN. ) SOLID_ANGLE_UNIT ( ) );
#14401=EDGE_CURVE ( 'NONE', #7933, #11794, #51, .T. ) ;
#14403=CARTESIAN_POINT ( 'NONE',  ( 109.4893729001365870, 209.7811923590224978, 348.0151256184570343 ) ) ;
#14404=FILL_AREA_STYLE_COLOUR ( '', #501 ) ;
#14409=DIRECTION ( 'NONE',  ( -9.815121534730717399E-17, 1.000000000000000000, -2.352167425053297897E-16 ) ) ;
#14430=FACE_OUTER_BOUND ( 'NONE', #15908, .T. ) ;
#14432=FILL_AREA_STYLE_COLOUR ( '', #15063 ) ;
#14441=CARTESIAN_POINT ( 'NONE',  ( 111.4893729001365870, 222.0013992467745823, 330.1364716053970483 ) ) ;
#14478=AXIS2_PLACEMENT_3D ( 'NONE', #19007, #20151, #4608 ) ;
#14487=FILL_AREA_STYLE_COLOUR ( '', #18461 ) ;
#14499=ORIENTED_EDGE ( 'NONE', *, *, #11001, .F. ) ;
#14506=( NAMED_UNIT ( * ) SI_UNIT ( $, .STERADIAN. ) SOLID_ANGLE_UNIT ( ) );
#14535=( GEOMETRIC_REPRESENTATION_CONTEXT ( 3 ) GLOBAL_UNCERTAINTY_ASSIGNED_CONTEXT ( ( #11973 ) ) GLOBAL_UNIT_ASSIGNED_CONTEXT ( ( #12051, #7700, #14389 ) ) REPRESENTATION_CONTEXT ( 'NONE', 'WORKASPACE' ) );
#14556=ORIENTED_EDGE ( 'NONE', *, *, #13174, .T. ) ;
#14585=DIRECTION ( 'NONE',  ( -0.000000000000000000, 0.7817866094812263578, 0.6235460666509320404 ) ) ;
#14597=ORIENTED_EDGE ( 'NONE', *, *, #11764, .F. ) ;
#14598=DIRECTION ( 'NONE',  ( 0.000000000000000000, 1.000000000000000000, 0.000000000000000000 ) ) ;
#14607=DIRECTION ( 'NONE',  ( 1.000000000000000000, 9.815121534730717399E-17, 0.000000000000000000 ) ) ;
#14608=DIRECTION ( 'NONE',  ( -6.120180426682198458E-17, 0.6235460666509320404, -0.7817866094812263578 ) ) ;
#14613=DIRECTION ( 'NONE',  ( 0.000000000000000000, 2.352167425053297897E-16, 1.000000000000000000 ) ) ;
#14614=MECHANICAL_DESIGN_GEOMETRIC_PRESENTATION_REPRESENTATION('',(#17950),#8041);
#14634=( GEOMETRIC_REPRESENTATION_CONTEXT ( 3 ) GLOBAL_UNCERTAINTY_ASSIGNED_CONTEXT ( ( #9910 ) ) GLOBAL_UNIT_ASSIGNED_CONTEXT ( ( #7028, #8364, #521 ) ) REPRESENTATION_CONTEXT ( 'NONE', 'WORKASPACE' ) );
#14642=DIRECTION ( 'NONE',  ( -5.827381659956976845E-17, 0.5937146717273790175, 0.8046756418431283420 ) ) ;
#14651=UNCERTAINTY_MEASURE_WITH_UNIT (LENGTH_MEASURE( 1.000000000000000082E-05 ), #15966, 'distance_accuracy_value', 'NONE');
#14673=FACE_BOUND ( 'NONE', #19972, .T. ) ;
#14684=EDGE_CURVE ( 'NONE', #15351, #7754, #2904, .T. ) ;
#14694=EDGE_CURVE ( 'NONE', #10459, #8530, #1035, .T. ) ;
#14708=ORIENTED_EDGE ( 'NONE', *, *, #17227, .F. ) ;
#14715=SURFACE_SIDE_STYLE ('',( #776 ) ) ;
#14726=( GEOMETRIC_REPRESENTATION_CONTEXT ( 3 ) GLOBAL_UNCERTAINTY_ASSIGNED_CONTEXT ( ( #5211 ) ) GLOBAL_UNIT_ASSIGNED_CONTEXT ( ( #3522, #3304, #15893 ) ) REPRESENTATION_CONTEXT ( 'NONE', 'WORKASPACE' ) );
#14733=CARTESIAN_POINT ( 'NONE',  ( 53.48937290013659407, 129.7247684487574588, 370.0000000000000000 ) ) ;
#14768=ORIENTED_EDGE ( 'NONE', *, *, #10339, .F. ) ;
#14775=CARTESIAN_POINT ( 'NONE',  ( 53.48937290013660828, 127.7247684487574304, 254.0000000000000000 ) ) ;
#14777=SURFACE_SIDE_STYLE ('',( #17563 ) ) ;
#14786=( NAMED_UNIT ( * ) PLANE_ANGLE_UNIT ( ) SI_UNIT ( $, .RADIAN. ) );
#14788=ADVANCED_FACE ( 'NONE', ( #20321, #17132, #4667 ), #10958, .F. ) ;
#14789=SURFACE_STYLE_USAGE ( .BOTH. , #17985 ) ;
#14805=ORIENTED_EDGE ( 'NONE', *, *, #14684, .T. ) ;
#14806=DIRECTION ( 'NONE',  ( -1.000000000000000000, -9.815121534730717399E-17, 0.000000000000000000 ) ) ;
#14867=FACE_OUTER_BOUND ( 'NONE', #2850, .T. ) ;
#14871=ORIENTED_EDGE ( 'NONE', *, *, #11764, .T. ) ;
#14886=DIRECTION ( 'NONE',  ( -0.000000000000000000, 0.7817866094812263578, 0.6235460666509320404 ) ) ;
#14900=PRODUCT_DEFINITION_FORMATION_WITH_SPECIFIED_SOURCE ( 'ANY', '', #17662, .NOT_KNOWN. ) ;
#14905=PRESENTATION_STYLE_ASSIGNMENT (( #9294 ) ) ;
#14912=SURFACE_STYLE_USAGE ( .BOTH. , #8615 ) ;
#14917=DIRECTION ( 'NONE',  ( 1.000000000000000000, 9.815121534730717399E-17, 0.000000000000000000 ) ) ;
#14931=VECTOR ( 'NONE', #15959, 1000.000000000000000 ) ;
#14940=EDGE_CURVE ( 'NONE', #10796, #2901, #13728, .T. ) ;
#14948=SURFACE_SIDE_STYLE ('',( #15141 ) ) ;
#14953=CIRCLE ( 'NONE', #3100, 2.000000000000001776 ) ;
#14956=LINE ( 'NONE', #2565, #1104 ) ;
#14972=CARTESIAN_POINT ( 'NONE',  ( 53.48937290013660828, 127.7247684487574304, 357.7985149490353933 ) ) ;
#15019=CARTESIAN_POINT ( 'NONE',  ( 111.4893729001366154, 77.72476844875745883, 250.0000000000000000 ) ) ;
#15029=FILL_AREA_STYLE_COLOUR ( '', #8324 ) ;
#15031=SURFACE_SIDE_STYLE ('',( #8748 ) ) ;
#15060=EDGE_CURVE ( 'NONE', #4349, #16025, #6109, .T. ) ;
#15063=COLOUR_RGB ( '', 0.08235294, 0.09019608, 0.10196078) ;
#15077=( NAMED_UNIT ( * ) PLANE_ANGLE_UNIT ( ) SI_UNIT ( $, .RADIAN. ) );
#15120=( NAMED_UNIT ( * ) SI_UNIT ( $, .STERADIAN. ) SOLID_ANGLE_UNIT ( ) );
#15121=CARTESIAN_POINT ( 'NONE',  ( 111.4893729001366012, 125.7247684487574588, 252.0000000000000000 ) ) ;
#15124=( NAMED_UNIT ( * ) PLANE_ANGLE_UNIT ( ) SI_UNIT ( $, .RADIAN. ) );
#15141=SURFACE_STYLE_FILL_AREA ( #18113 ) ;
#15150=ORIENTED_EDGE ( 'NONE', *, *, #6858, .T. ) ;
#15160=DIRECTION ( 'NONE',  ( -6.120180426682197225E-17, 0.6235460666509320404, -0.7817866094812263578 ) ) ;
#15167=DIRECTION ( 'NONE',  ( 0.000000000000000000, -2.352167425053297897E-16, -1.000000000000000000 ) ) ;
#15168=DIRECTION ( 'NONE',  ( -1.000000000000000000, -9.815121534730717399E-17, 0.000000000000000000 ) ) ;
#15183=DIRECTION ( 'NONE',  ( 1.000000000000000000, 9.815121534730717399E-17, 0.000000000000000000 ) ) ;
#15214=PRESENTATION_STYLE_ASSIGNMENT (( #3031 ) ) ;
#15216=CIRCLE ( 'NONE', #14224, 2.000000000000001776 ) ;
#15219=( GEOMETRIC_REPRESENTATION_CONTEXT ( 3 ) GLOBAL_UNCERTAINTY_ASSIGNED_CONTEXT ( ( #2699 ) ) GLOBAL_UNIT_ASSIGNED_CONTEXT ( ( #8225, #19335, #11513 ) ) REPRESENTATION_CONTEXT ( 'NONE', 'WORKASPACE' ) );
#15237=AXIS2_PLACEMENT_3D ( 'NONE', #11487, #3663, #8413 ) ;
#15240=ORIENTED_EDGE ( 'NONE', *, *, #14684, .F. ) ;
#15265=UNCERTAINTY_MEASURE_WITH_UNIT (LENGTH_MEASURE( 1.000000000000000082E-05 ), #2905, 'distance_accuracy_value', 'NONE');
#15278=DIRECTION ( 'NONE',  ( 1.000000000000000000, 9.815121534730717399E-17, 0.000000000000000000 ) ) ;
#15283=VECTOR ( 'NONE', #12007, 1000.000000000000000 ) ;
#15289=UNCERTAINTY_MEASURE_WITH_UNIT (LENGTH_MEASURE( 1.000000000000000082E-05 ), #4292, 'distance_accuracy_value', 'NONE');
#15290=ADVANCED_FACE ( 'NONE', ( #5246 ), #3694, .T. ) ;
#15292=MECHANICAL_DESIGN_GEOMETRIC_PRESENTATION_REPRESENTATION('',(#8697),#13321);
#15333=FACE_OUTER_BOUND ( 'NONE', #2825, .T. ) ;
#15342=FILL_AREA_STYLE ('',( #2443 ) ) ;
#15351=VERTEX_POINT ( 'NONE', #18000 ) ;
#15424=DIRECTION ( 'NONE',  ( -1.000000000000000000, 0.000000000000000000, 0.000000000000000000 ) ) ;
#15452=EDGE_LOOP ( 'NONE', ( #10346, #13512, #15554, #17990, #2445, #20077 ) ) ;
#15462=( NAMED_UNIT ( * ) PLANE_ANGLE_UNIT ( ) SI_UNIT ( $, .RADIAN. ) );
#15468=ORIENTED_EDGE ( 'NONE', *, *, #12413, .F. ) ;
#15496=EDGE_CURVE ( 'NONE', #323, #9433, #4605, .T. ) ;
#15541=COLOUR_RGB ( '', 0.08235294, 0.09019608, 0.10196078) ;
#15547=FILL_AREA_STYLE ('',( #17169 ) ) ;
#15554=ORIENTED_EDGE ( 'NONE', *, *, #11001, .T. ) ;
#15570=( GEOMETRIC_REPRESENTATION_CONTEXT ( 3 ) GLOBAL_UNCERTAINTY_ASSIGNED_CONTEXT ( ( #16519 ) ) GLOBAL_UNIT_ASSIGNED_CONTEXT ( ( #13685, #15124, #3995 ) ) REPRESENTATION_CONTEXT ( 'NONE', 'WORKASPACE' ) );
#15602=LINE ( 'NONE', #5071, #8384 ) ;
#15610=LINE ( 'NONE', #4466, #8888 ) ;
#15615=MECHANICAL_DESIGN_GEOMETRIC_PRESENTATION_REPRESENTATION('',(#9341),#17239);
#15619=FACE_OUTER_BOUND ( 'NONE', #6737, .T. ) ;
#15644=SURFACE_SIDE_STYLE ('',( #9327 ) ) ;
#15645=STYLED_ITEM ( 'NONE', ( #4874 ), #10404 ) ;
#15650=ORIENTED_EDGE ( 'NONE', *, *, #13024, .T. ) ;
#15660=ORIENTED_EDGE ( 'NONE', *, *, #10339, .T. ) ;
#15668=SURFACE_SIDE_STYLE ('',( #18927 ) ) ;
#15687=ORIENTED_EDGE ( 'NONE', *, *, #18666, .F. ) ;
#15696=AXIS2_PLACEMENT_3D ( 'NONE', #7534, #7834, #8963 ) ;
#15721=DIRECTION ( 'NONE',  ( 0.000000000000000000, 0.000000000000000000, 1.000000000000000000 ) ) ;
#15732=VERTEX_POINT ( 'NONE', #4167 ) ;
#15742=EDGE_LOOP ( 'NONE', ( #5757, #5950, #17841, #14556 ) ) ;
#15751=SURFACE_STYLE_FILL_AREA ( #14079 ) ;
#15775=DIRECTION ( 'NONE',  ( 1.000000000000000000, 6.763469278324249959E-16, 4.651923389110021175E-16 ) ) ;
#15779=UNCERTAINTY_MEASURE_WITH_UNIT (LENGTH_MEASURE( 1.000000000000000082E-05 ), #7156, 'distance_accuracy_value', 'NONE');
#15813=DIRECTION ( 'NONE',  ( 0.000000000000000000, 0.000000000000000000, -1.000000000000000000 ) ) ;
#15814=CARTESIAN_POINT ( 'NONE',  ( 108.9893729001366154, 131.2883416677199193, 282.8521325859589979 ) ) ;
#15832=CARTESIAN_POINT ( 'NONE',  ( 53.48937290013659407, 129.7247684487574588, 368.0000000000000000 ) ) ;
#15862=FACE_OUTER_BOUND ( 'NONE', #9813, .T. ) ;
#15886=CARTESIAN_POINT ( 'NONE',  ( 53.48937290013659407, 127.7247684487574304, 250.0000000000000000 ) ) ;
#15893=( NAMED_UNIT ( * ) SI_UNIT ( $, .STERADIAN. ) SOLID_ANGLE_UNIT ( ) );
#15898=STYLED_ITEM ( 'NONE', ( #7684 ), #8261 ) ;
#15908=EDGE_LOOP ( 'NONE', ( #15660, #14215, #12053, #17624 ) ) ;
#15910=( NAMED_UNIT ( * ) PLANE_ANGLE_UNIT ( ) SI_UNIT ( $, .RADIAN. ) );
#15955=ORIENTED_EDGE ( 'NONE', *, *, #5922, .T. ) ;
#15956=DIRECTION ( 'NONE',  ( -9.815121534730718631E-17, 1.000000000000000000, 0.000000000000000000 ) ) ;
#15959=DIRECTION ( 'NONE',  ( 2.597405907254919044E-19, 0.7791332379872890623, 0.6268583551835632539 ) ) ;
#15966=( LENGTH_UNIT ( ) NAMED_UNIT ( * ) SI_UNIT ( .MILLI., .METRE. ) );
#15967=MECHANICAL_DESIGN_GEOMETRIC_PRESENTATION_REPRESENTATION('',(#8383),#782);
#15976=VECTOR ( 'NONE', #19015, 1000.000000000000000 ) ;
#15983=PLANE ( 'NONE',  #20211 ) ;
#15991=DIRECTION ( 'NONE',  ( 0.000000000000000000, 0.000000000000000000, 1.000000000000000000 ) ) ;
#16014=ADVANCED_FACE ( 'NONE', ( #19566 ), #610, .T. ) ;
#16018=SURFACE_STYLE_FILL_AREA ( #6829 ) ;
#16025=VERTEX_POINT ( 'NONE', #10415 ) ;
#16030=ORIENTED_EDGE ( 'NONE', *, *, #10828, .T. ) ;
#16063=CARTESIAN_POINT ( 'NONE',  ( 55.98937290013660828, 130.3113892758443058, 284.0770112900635240 ) ) ;
#16089=( NAMED_UNIT ( * ) PLANE_ANGLE_UNIT ( ) SI_UNIT ( $, .RADIAN. ) );
#16090=EDGE_CURVE ( 'NONE', #16423, #12769, #4938, .T. ) ;
#16102=ORIENTED_EDGE ( 'NONE', *, *, #19885, .F. ) ;
#16113=DIRECTION ( 'NONE',  ( 1.000000000000000000, 9.815121534730718631E-17, -0.000000000000000000 ) ) ;
#16121=DIRECTION ( 'NONE',  ( 0.000000000000000000, -1.000000000000000000, 0.000000000000000000 ) ) ;
#16131=DIRECTION ( 'NONE',  ( -9.815121534730717399E-17, 1.000000000000000000, 0.000000000000000000 ) ) ;
#16147=ORIENTED_EDGE ( 'NONE', *, *, #15496, .F. ) ;
#16167=LINE ( 'NONE', #9754, #2716 ) ;
#16187=MECHANICAL_DESIGN_GEOMETRIC_PRESENTATION_REPRESENTATION('',(#11208),#4643);
#16188=FILL_AREA_STYLE ('',( #11314 ) ) ;
#16196=EDGE_CURVE ( 'NONE', #2417, #3307, #790, .T. ) ;
#16201=FILL_AREA_STYLE ('',( #802 ) ) ;
#16209=SURFACE_SIDE_STYLE ('',( #16018 ) ) ;
#16222=ORIENTED_EDGE ( 'NONE', *, *, #16090, .F. ) ;
#16232=( NAMED_UNIT ( * ) PLANE_ANGLE_UNIT ( ) SI_UNIT ( $, .RADIAN. ) );
#16236=VECTOR ( 'NONE', #11516, 1000.000000000000000 ) ;
#16281=ORIENTED_EDGE ( 'NONE', *, *, #14401, .T. ) ;
#16293=EDGE_LOOP ( 'NONE', ( #20358, #17804, #10975, #11658 ) ) ;
#16306=DIRECTION ( 'NONE',  ( 6.152690941188070202E-17, -0.6268583551835633649, 0.7791332379872890623 ) ) ;
#16307=AXIS2_PLACEMENT_3D ( 'NONE', #2358, #13214, #5564 ) ;
#16310=VECTOR ( 'NONE', #19884, 1000.000000000000000 ) ;
#16316=( GEOMETRIC_REPRESENTATION_CONTEXT ( 3 ) GLOBAL_UNCERTAINTY_ASSIGNED_CONTEXT ( ( #18061 ) ) GLOBAL_UNIT_ASSIGNED_CONTEXT ( ( #2012, #4837, #14305 ) ) REPRESENTATION_CONTEXT ( 'NONE', 'WORKASPACE' ) );
#16326=SURFACE_STYLE_FILL_AREA ( #6626 ) ;
#16327=UNCERTAINTY_MEASURE_WITH_UNIT (LENGTH_MEASURE( 1.000000000000000082E-05 ), #17609, 'distance_accuracy_value', 'NONE');
#16328=ORIENTED_EDGE ( 'NONE', *, *, #6858, .F. ) ;
#16358=VERTEX_POINT ( 'NONE', #885 ) ;
#16362=AXIS2_PLACEMENT_3D ( 'NONE', #2466, #10409, #9066 ) ;
#16383=ORIENTED_EDGE ( 'NONE', *, *, #2921, .T. ) ;
#16385=CARTESIAN_POINT ( 'NONE',  ( 111.4893729001366154, 77.72476844875745883, 252.0000000000000000 ) ) ;
#16397=ADVANCED_FACE ( 'NONE', ( #14284 ), #9540, .F. ) ;
#16423=VERTEX_POINT ( 'NONE', #9340 ) ;
#16424=CARTESIAN_POINT ( 'NONE',  ( 55.98937290013660828, 95.58236431990633264, 327.6194023385999685 ) ) ;
#16452=ADVANCED_FACE ( 'NONE', ( #18623 ), #2945, .T. ) ;
#16462=EDGE_CURVE ( 'NONE', #258, #7981, #19117, .T. ) ;
#16485=UNCERTAINTY_MEASURE_WITH_UNIT (LENGTH_MEASURE( 1.000000000000000082E-05 ), #17685, 'distance_accuracy_value', 'NONE');
#16499=DIRECTION ( 'NONE',  ( -1.314570224013242627E-15, 1.000000000000000000, 0.000000000000000000 ) ) ;
#16514=UNCERTAINTY_MEASURE_WITH_UNIT (LENGTH_MEASURE( 1.000000000000000082E-05 ), #11193, 'distance_accuracy_value', 'NONE');
#16519=UNCERTAINTY_MEASURE_WITH_UNIT (LENGTH_MEASURE( 1.000000000000000082E-05 ), #13685, 'distance_accuracy_value', 'NONE');
#16525=VECTOR ( 'NONE', #17378, 1000.000000000000227 ) ;
#16526=DIRECTION ( 'NONE',  ( 1.000000000000000000, 9.815121534730717399E-17, -0.000000000000000000 ) ) ;
#16541=ORIENTED_EDGE ( 'NONE', *, *, #7976, .T. ) ;
#16579=SURFACE_SIDE_STYLE ('',( #2636 ) ) ;
#16588=UNCERTAINTY_MEASURE_WITH_UNIT (LENGTH_MEASURE( 1.000000000000000082E-05 ), #3892, 'distance_accuracy_value', 'NONE');
#16592=ORIENTED_EDGE ( 'NONE', *, *, #9927, .F. ) ;
#16594=ORIENTED_EDGE ( 'NONE', *, *, #4148, .F. ) ;
#16605=SURFACE_SIDE_STYLE ('',( #6072 ) ) ;
#16626=EDGE_LOOP ( 'NONE', ( #13372, #17435, #18979, #2142 ) ) ;
#16639=MECHANICAL_DESIGN_GEOMETRIC_PRESENTATION_REPRESENTATION('',(#1448),#4122);
#16642=DIRECTION ( 'NONE',  ( 0.000000000000000000, -0.7699350945217658948, -0.6381222063396316813 ) ) ;
#16644=VECTOR ( 'NONE', #19107, 1000.000000000000000 ) ;
#16646=DIRECTION ( 'NONE',  ( 1.000000000000000000, 9.815121534730717399E-17, 0.000000000000000000 ) ) ;
#16658=DIRECTION ( 'NONE',  ( 0.000000000000000000, 1.000000000000000000, 0.000000000000000000 ) ) ;
#16665=ORIENTED_EDGE ( 'NONE', *, *, #1672, .F. ) ;
#16708=CYLINDRICAL_SURFACE ( 'NONE', #19176, 3.283624802691453848 ) ;
#16711=DIRECTION ( 'NONE',  ( -0.000000000000000000, -0.000000000000000000, 1.000000000000000000 ) ) ;
#16757=DIRECTION ( 'NONE',  ( 1.000000000000000000, 9.815121534730717399E-17, 0.000000000000000000 ) ) ;
#16852=DIRECTION ( 'NONE',  ( 1.000000000000000000, 9.815121534730717399E-17, 0.000000000000000000 ) ) ;
#16895=VERTEX_POINT ( 'NONE', #1337 ) ;
#16901=LINE ( 'NONE', #6279, #13799 ) ;
#16906=EDGE_CURVE ( 'NONE', #6446, #258, #9714, .T. ) ;
#16912=DIRECTION ( 'NONE',  ( -1.000000000000000000, -9.815121534730717399E-17, 0.000000000000000000 ) ) ;
#16918=UNCERTAINTY_MEASURE_WITH_UNIT (LENGTH_MEASURE( 1.000000000000000082E-05 ), #3480, 'distance_accuracy_value', 'NONE');
#16950=CARTESIAN_POINT ( 'NONE',  ( 111.4893729001366154, 77.72476844875745883, 252.0000000000000000 ) ) ;
#16977=FACE_OUTER_BOUND ( 'NONE', #16293, .T. ) ;
#17000=VECTOR ( 'NONE', #15160, 1000.000000000000227 ) ;
#17027=CARTESIAN_POINT ( 'NONE',  ( 53.48937290013659407, 129.7247684487574304, 281.6050404526570219 ) ) ;
#17045=CARTESIAN_POINT ( 'NONE',  ( -77.99033078109006567, 49.66333933884486385, 252.0000000000000000 ) ) ;
#17078=ORIENTED_EDGE ( 'NONE', *, *, #7049, .F. ) ;
#17105=STYLED_ITEM ( 'NONE', ( #20354 ), #16452 ) ;
#17112=CARTESIAN_POINT ( 'NONE',  ( 53.48937290013659407, 209.5175665826582474, 345.1990110167342891 ) ) ;
#17132=FACE_BOUND ( 'NONE', #2544, .T. ) ;
#17142=ORIENTED_EDGE ( 'NONE', *, *, #9289, .T. ) ;
#17151=VERTEX_POINT ( 'NONE', #2668 ) ;
#17155=ADVANCED_FACE ( 'NONE', ( #5664 ), #12154, .T. ) ;
#17157=LINE ( 'NONE', #1165, #491 ) ;
#17169=FILL_AREA_STYLE_COLOUR ( '', #639 ) ;
#17174=EDGE_LOOP ( 'NONE', ( #12567, #12187, #15150, #9441 ) ) ;
#17180=CARTESIAN_POINT ( 'NONE',  ( 53.48937290013658696, 122.8810204491430369, 322.0399576098686225 ) ) ;
#17186=( LENGTH_UNIT ( ) NAMED_UNIT ( * ) SI_UNIT ( .MILLI., .METRE. ) );
#17206=VECTOR ( 'NONE', #14339, 1000.000000000000000 ) ;
#17227=EDGE_CURVE ( 'NONE', #2567, #2573, #17614, .T. ) ;
#17236=CARTESIAN_POINT ( 'NONE',  ( 111.4893729001366012, 129.7247684487574304, 252.0000000000000000 ) ) ;
#17238=ADVANCED_BREP_SHAPE_REPRESENTATION ( '', ( #8261, #8166, #2741 ), #5024 ) ;
#17239=( GEOMETRIC_REPRESENTATION_CONTEXT ( 3 ) GLOBAL_UNCERTAINTY_ASSIGNED_CONTEXT ( ( #2257 ) ) GLOBAL_UNIT_ASSIGNED_CONTEXT ( ( #17186, #12363, #7917 ) ) REPRESENTATION_CONTEXT ( 'NONE', 'WORKASPACE' ) );
#17241=FILL_AREA_STYLE_COLOUR ( '', #4799 ) ;
#17247=CARTESIAN_POINT ( 'NONE',  ( 53.48937290013659407, 210.4096692328538154, 345.9586017849865129 ) ) ;
#17248=CARTESIAN_POINT ( 'NONE',  ( 111.4893729001366012, 127.7247684487574588, 357.7985149490353933 ) ) ;
#17255=EDGE_LOOP ( 'NONE', ( #12784, #13422, #5885, #3902, #17498, #16222 ) ) ;
#17272=FACE_OUTER_BOUND ( 'NONE', #18286, .T. ) ;
#17273=ORIENTED_EDGE ( 'NONE', *, *, #5374, .T. ) ;
#17280=LINE ( 'NONE', #12539, #16525 ) ;
#17290=FILL_AREA_STYLE ('',( #3057 ) ) ;
#17295=CYLINDRICAL_SURFACE ( 'NONE', #4684, 2.000000000000001776 ) ;
#17297=SURFACE_STYLE_USAGE ( .BOTH. , #9871 ) ;
#17337=CYLINDRICAL_SURFACE ( 'NONE', #3450, 1.999999999999997113 ) ;
#17350=MECHANICAL_DESIGN_GEOMETRIC_PRESENTATION_REPRESENTATION('',(#18331),#14726);
#17355=EDGE_LOOP ( 'NONE', ( #11721, #13000, #18433, #13934 ) ) ;
#17364=FILL_AREA_STYLE_COLOUR ( '', #19166 ) ;
#17365=VECTOR ( 'NONE', #11619, 1000.000000000000000 ) ;
#17378=DIRECTION ( 'NONE',  ( 1.632680918566406990E-15, -0.7817866094812271349, -0.6235460666509309302 ) ) ;
#17396=CARTESIAN_POINT ( 'NONE',  ( 108.9893729001365870, 143.5567736071463969, 294.7336993003747239 ) ) ;
#17416=AXIS2_PLACEMENT_3D ( 'NONE', #9138, #7593, #20147 ) ;
#17435=ORIENTED_EDGE ( 'NONE', *, *, #407, .F. ) ;
#17456=( LENGTH_UNIT ( ) NAMED_UNIT ( * ) SI_UNIT ( .MILLI., .METRE. ) );
#17468=CARTESIAN_POINT ( 'NONE',  ( 53.48937290013659407, 209.7811923590224978, 348.0151256184570343 ) ) ;
#17482=( LENGTH_UNIT ( ) NAMED_UNIT ( * ) SI_UNIT ( .MILLI., .METRE. ) );
#17497=ORIENTED_EDGE ( 'NONE', *, *, #5983, .F. ) ;
#17498=ORIENTED_EDGE ( 'NONE', *, *, #12519, .F. ) ;
#17542=ADVANCED_FACE ( 'NONE', ( #9043 ), #5945, .T. ) ;
#17549=EDGE_CURVE ( 'NONE', #3307, #15732, #17280, .T. ) ;
#17563=SURFACE_STYLE_FILL_AREA ( #11276 ) ;
#17598=VECTOR ( 'NONE', #11157, 1000.000000000000000 ) ;
#17605=EDGE_CURVE ( 'NONE', #17151, #4707, #10790, .T. ) ;
#17609=( LENGTH_UNIT ( ) NAMED_UNIT ( * ) SI_UNIT ( .MILLI., .METRE. ) );
#17614=LINE ( 'NONE', #17396, #12206 ) ;
#17624=ORIENTED_EDGE ( 'NONE', *, *, #5701, .F. ) ;
#17640=CARTESIAN_POINT ( 'NONE',  ( 111.4893729001366012, 127.7247684487574304, 252.0000000000000000 ) ) ;
#17653=SURFACE_SIDE_STYLE ('',( #8282 ) ) ;
#17662=PRODUCT ( 'Part14', 'Part14', '', ( #4188 ) ) ;
#17683=CARTESIAN_POINT ( 'NONE',  ( 111.4893729001365870, 209.1356689931817812, 347.4957642363283412 ) ) ;
#17685=( LENGTH_UNIT ( ) NAMED_UNIT ( * ) SI_UNIT ( .MILLI., .METRE. ) );
#17700=CARTESIAN_POINT ( 'NONE',  ( 53.48937290013658696, 126.1646452518344859, 280.0825295754780768 ) ) ;
#17743=UNCERTAINTY_MEASURE_WITH_UNIT (LENGTH_MEASURE( 1.000000000000000082E-05 ), #2162, 'distance_accuracy_value', 'NONE');
#17751=SURFACE_SIDE_STYLE ('',( #5197 ) ) ;
#17761=ADVANCED_FACE ( 'NONE', ( #13167 ), #11601, .T. ) ;
#17765=UNCERTAINTY_MEASURE_WITH_UNIT (LENGTH_MEASURE( 1.000000000000000082E-05 ), #10329, 'distance_accuracy_value', 'NONE');
#17769=FILL_AREA_STYLE_COLOUR ( '', #1047 ) ;
#17781=CARTESIAN_POINT ( 'NONE',  ( 55.48937290013659407, 209.7811923590224978, 348.0151256184570343 ) ) ;
#17783=ORIENTED_EDGE ( 'NONE', *, *, #16462, .F. ) ;
#17785=VECTOR ( 'NONE', #17955, 1000.000000000000000 ) ;
#17804=ORIENTED_EDGE ( 'NONE', *, *, #7976, .F. ) ;
#17828=CARTESIAN_POINT ( 'NONE',  ( 111.4893729001366154, 77.72476844875745883, 250.0000000000000000 ) ) ;
#17832=FACE_OUTER_BOUND ( 'NONE', #2524, .T. ) ;
#17841=ORIENTED_EDGE ( 'NONE', *, *, #3173, .T. ) ;
#17845=MECHANICAL_DESIGN_GEOMETRIC_PRESENTATION_REPRESENTATION('',(#71),#18482);
#17846=EDGE_CURVE ( 'NONE', #9405, #15351, #13961, .T. ) ;
#17848=FACE_OUTER_BOUND ( 'NONE', #16626, .T. ) ;
#17881=FILL_AREA_STYLE ('',( #14487 ) ) ;
#17916=EDGE_CURVE ( 'NONE', #4707, #7627, #15216, .T. ) ;
#17917=AXIS2_PLACEMENT_3D ( 'NONE', #8925, #2326, #18303 ) ;
#17929=CARTESIAN_POINT ( 'NONE',  ( 111.4893729001366012, 125.7247684487574588, 254.0000000000000000 ) ) ;
#17932=VECTOR ( 'NONE', #1141, 1000.000000000000000 ) ;
#17950=STYLED_ITEM ( 'NONE', ( #1961 ), #14788 ) ;
#17953=FILL_AREA_STYLE ('',( #19297 ) ) ;
#17955=DIRECTION ( 'NONE',  ( -1.824549968389412905E-16, 1.000000000000000000, 0.000000000000000000 ) ) ;
#17985=SURFACE_SIDE_STYLE ('',( #2206 ) ) ;
#17990=ORIENTED_EDGE ( 'NONE', *, *, #2812, .T. ) ;
#17997=( NAMED_UNIT ( * ) PLANE_ANGLE_UNIT ( ) SI_UNIT ( $, .RADIAN. ) );
#18000=CARTESIAN_POINT ( 'NONE',  ( 53.48937290013660117, 77.72476844875745883, 250.0000000000000000 ) ) ;
#18001=DIRECTION ( 'NONE',  ( 1.000000000000000000, 9.815121534730718631E-17, 0.000000000000000000 ) ) ;
#18014=( NAMED_UNIT ( * ) PLANE_ANGLE_UNIT ( ) SI_UNIT ( $, .RADIAN. ) );
#18024=CARTESIAN_POINT ( 'NONE',  ( 53.48937290013658696, 119.5973956464515879, 280.0825295754780768 ) ) ;
#18061=UNCERTAINTY_MEASURE_WITH_UNIT (LENGTH_MEASURE( 1.000000000000000082E-05 ), #2012, 'distance_accuracy_value', 'NONE');
#18079=VERTEX_POINT ( 'NONE', #18094 ) ;
#18081=DIRECTION ( 'NONE',  ( -9.815121534730717399E-17, 1.000000000000000000, 0.000000000000000000 ) ) ;
#18084=( GEOMETRIC_REPRESENTATION_CONTEXT ( 3 ) GLOBAL_UNCERTAINTY_ASSIGNED_CONTEXT ( ( #16588 ) ) GLOBAL_UNIT_ASSIGNED_CONTEXT ( ( #3892, #17997, #13389 ) ) REPRESENTATION_CONTEXT ( 'NONE', 'WORKASPACE' ) );
#18088=DIRECTION ( 'NONE',  ( -1.000000000000000000, 0.000000000000000000, -0.000000000000000000 ) ) ;
#18089=CARTESIAN_POINT ( 'NONE',  ( 111.4893729001366012, 122.8810204491430369, 322.0399576098686225 ) ) ;
#18091=SURFACE_STYLE_USAGE ( .BOTH. , #16579 ) ;
#18094=CARTESIAN_POINT ( 'NONE',  ( 109.4893729001365870, 211.0574367717017594, 346.4752554294135507 ) ) ;
#18113=FILL_AREA_STYLE ('',( #8652 ) ) ;
#18127=VERTEX_POINT ( 'NONE', #19938 ) ;
#18128=VERTEX_POINT ( 'NONE', #2539 ) ;
#18178=VECTOR ( 'NONE', #15168, 1000.000000000000000 ) ;
#18200=SURFACE_STYLE_FILL_AREA ( #5542 ) ;
#18255=LINE ( 'NONE', #8794, #338 ) ;
#18262=AXIS2_PLACEMENT_3D ( 'NONE', #17640, #9812, #16121 ) ;
#18266=AXIS2_PLACEMENT_3D ( 'NONE', #2177, #16526, #16131 ) ;
#18286=EDGE_LOOP ( 'NONE', ( #7911, #11477, #18878, #13910 ) ) ;
#18303=DIRECTION ( 'NONE',  ( 0.000000000000000000, 0.6235460666509320404, -0.7817866094812263578 ) ) ;
#18313=EDGE_CURVE ( 'NONE', #12074, #12831, #16167, .T. ) ;
#18327=SURFACE_STYLE_FILL_AREA ( #10598 ) ;
#18331=STYLED_ITEM ( 'NONE', ( #14222 ), #3760 ) ;
#18353=FILL_AREA_STYLE ('',( #5095 ) ) ;
#18359=UNCERTAINTY_MEASURE_WITH_UNIT (LENGTH_MEASURE( 1.000000000000000082E-05 ), #1504, 'distance_accuracy_value', 'NONE');
#18420=SURFACE_SIDE_STYLE ('',( #18327 ) ) ;
#18433=ORIENTED_EDGE ( 'NONE', *, *, #12804, .T. ) ;
#18452=( NAMED_UNIT ( * ) SI_UNIT ( $, .STERADIAN. ) SOLID_ANGLE_UNIT ( ) );
#18461=COLOUR_RGB ( '', 0.09019608, 0.27058824, 0.51372549) ;
#18482=( GEOMETRIC_REPRESENTATION_CONTEXT ( 3 ) GLOBAL_UNCERTAINTY_ASSIGNED_CONTEXT ( ( #18359 ) ) GLOBAL_UNIT_ASSIGNED_CONTEXT ( ( #1504, #275, #9551 ) ) REPRESENTATION_CONTEXT ( 'NONE', 'WORKASPACE' ) );
#18504=AXIS2_PLACEMENT_3D ( 'NONE', #19891, #4451, #16642 ) ;
#18542=UNCERTAINTY_MEASURE_WITH_UNIT (LENGTH_MEASURE( 1.000000000000000082E-05 ), #9073, 'distance_accuracy_value', 'NONE');
#18563=AXIS2_PLACEMENT_3D ( 'NONE', #12688, #16912, #10722 ) ;
#18564=VECTOR ( 'NONE', #18746, 1000.000000000000000 ) ;
#18567=CIRCLE ( 'NONE', #9693, 3.283624802691453848 ) ;
#18575=CARTESIAN_POINT ( 'NONE',  ( 53.48937290013658696, 119.5973956464515879, 280.0825295754780768 ) ) ;
#18623=FACE_OUTER_BOUND ( 'NONE', #12763, .T. ) ;
#18625=VECTOR ( 'NONE', #6298, 1000.000000000000000 ) ;
#18644=SURFACE_STYLE_FILL_AREA ( #5972 ) ;
#18660=CARTESIAN_POINT ( 'NONE',  ( 53.48937290013660828, 127.7247684487574304, 357.7985149490353933 ) ) ;
#18666=EDGE_CURVE ( 'NONE', #10931, #4636, #13872, .T. ) ;
#18667=VECTOR ( 'NONE', #8946, 1000.000000000000000 ) ;
#18675=CARTESIAN_POINT ( 'NONE',  ( 111.4893729001366154, 77.72476844875745883, 252.0000000000000000 ) ) ;
#18677=VECTOR ( 'NONE', #12414, 1000.000000000000000 ) ;
#18696=ORIENTED_EDGE ( 'NONE', *, *, #14694, .T. ) ;
#18701=FILL_AREA_STYLE ('',( #6157 ) ) ;
#18715=ORIENTED_EDGE ( 'NONE', *, *, #14371, .F. ) ;
#18746=DIRECTION ( 'NONE',  ( -6.263247009234063646E-17, 0.6381222063396385646, -0.7699350945217602327 ) ) ;
#18752=EDGE_CURVE ( 'NONE', #4636, #2567, #9639, .T. ) ;
#18767=SURFACE_STYLE_FILL_AREA ( #1543 ) ;
#18775=PRESENTATION_STYLE_ASSIGNMENT (( #7664 ) ) ;
#18792=SURFACE_SIDE_STYLE ('',( #7582 ) ) ;
#18806=ORIENTED_EDGE ( 'NONE', *, *, #7490, .F. ) ;
#18817=COLOUR_RGB ( '', 0.66274510, 0.83137255, 0.94901961) ;
#18878=ORIENTED_EDGE ( 'NONE', *, *, #5591, .T. ) ;
#18886=DIRECTION ( 'NONE',  ( 9.815121534730717399E-17, -1.000000000000000000, 0.000000000000000000 ) ) ;
#18927=SURFACE_STYLE_FILL_AREA ( #17290 ) ;
#18928=FILL_AREA_STYLE ('',( #12664 ) ) ;
#18933=PLANE ( 'NONE',  #8415 ) ;
#18957=( GEOMETRIC_REPRESENTATION_CONTEXT ( 3 ) GLOBAL_UNCERTAINTY_ASSIGNED_CONTEXT ( ( #19581 ) ) GLOBAL_UNIT_ASSIGNED_CONTEXT ( ( #4229, #899, #4133 ) ) REPRESENTATION_CONTEXT ( 'NONE', 'WORKASPACE' ) );
#18968=EDGE_CURVE ( 'NONE', #16895, #7678, #6387, .T. ) ;
#18979=ORIENTED_EDGE ( 'NONE', *, *, #11946, .F. ) ;
#18988=ORIENTED_EDGE ( 'NONE', *, *, #14694, .F. ) ;
#18995=AXIS2_PLACEMENT_3D ( 'NONE', #5154, #5041, #15991 ) ;
#19007=CARTESIAN_POINT ( 'NONE',  ( 53.48937290013658696, 122.8810204491430369, 322.0399576098686225 ) ) ;
#19015=DIRECTION ( 'NONE',  ( 1.000000000000000000, 9.815121534730718631E-17, 0.000000000000000000 ) ) ;
#19016=CYLINDRICAL_SURFACE ( 'NONE', #9957, 3.283624802691453848 ) ;
#19032=UNCERTAINTY_MEASURE_WITH_UNIT (LENGTH_MEASURE( 1.000000000000000082E-05 ), #13935, 'distance_accuracy_value', 'NONE');
#19038=VERTEX_POINT ( 'NONE', #17248 ) ;
#19062=MECHANICAL_DESIGN_GEOMETRIC_PRESENTATION_REPRESENTATION('',(#11857),#10522);
#19067=ORIENTED_EDGE ( 'NONE', *, *, #1672, .T. ) ;
#19102=EDGE_LOOP ( 'NONE', ( #2807, #14069, #18696, #4280 ) ) ;
#19107=DIRECTION ( 'NONE',  ( -1.000000000000000000, -9.815121534730717399E-17, 0.000000000000000000 ) ) ;
#19117=LINE ( 'NONE', #17781, #3946 ) ;
#19128=DIRECTION ( 'NONE',  ( 1.000000000000000000, 0.000000000000000000, -0.000000000000000000 ) ) ;
#19130=CARTESIAN_POINT ( 'NONE',  ( 111.4893729001366012, 125.7247684487574588, 254.0000000000000000 ) ) ;
#19141=ORIENTED_EDGE ( 'NONE', *, *, #14401, .F. ) ;
#19149=VERTEX_POINT ( 'NONE', #638 ) ;
#19166=COLOUR_RGB ( '', 0.66274510, 0.83137255, 0.94901961) ;
#19170=COLOUR_RGB ( '', 0.40784314, 0.44705882, 0.49803922) ;
#19176=AXIS2_PLACEMENT_3D ( 'NONE', #17180, #20365, #2957 ) ;
#19186=COLOUR_RGB ( '', 0.66274510, 0.83137255, 0.94901961) ;
#19194=PLANE ( 'NONE',  #2597 ) ;
#19226=DIRECTION ( 'NONE',  ( 0.000000000000000000, 0.000000000000000000, 1.000000000000000000 ) ) ;
#19229=SURFACE_STYLE_USAGE ( .BOTH. , #8208 ) ;
#19236=DIRECTION ( 'NONE',  ( -1.000000000000000000, -9.815121534730717399E-17, 0.000000000000000000 ) ) ;
#19257=FILL_AREA_STYLE ('',( #14404 ) ) ;
#19286=SURFACE_STYLE_USAGE ( .BOTH. , #9909 ) ;
#19297=FILL_AREA_STYLE_COLOUR ( '', #19170 ) ;
#19310=DIRECTION ( 'NONE',  ( -6.120180426682197225E-17, 0.6235460666509320404, -0.7817866094812263578 ) ) ;
#19331=APPLICATION_CONTEXT ( 'automotive_design' ) ;
#19335=( NAMED_UNIT ( * ) PLANE_ANGLE_UNIT ( ) SI_UNIT ( $, .RADIAN. ) );
#19343=CARTESIAN_POINT ( 'NONE',  ( -77.99033078109006567, 49.66333933884486385, 252.0000000000000000 ) ) ;
#19346=DIRECTION ( 'NONE',  ( 1.000000000000000000, 1.047380211910525299E-15, -0.000000000000000000 ) ) ;
#19386=CYLINDRICAL_SURFACE ( 'NONE', #18504, 1.999999999999997113 ) ;
#19394=ORIENTED_EDGE ( 'NONE', *, *, #14289, .F. ) ;
#19395=MECHANICAL_DESIGN_GEOMETRIC_PRESENTATION_REPRESENTATION('',(#17105),#1952);
#19397=ORIENTED_EDGE ( 'NONE', *, *, #6833, .T. ) ;
#19405=( LENGTH_UNIT ( ) NAMED_UNIT ( * ) SI_UNIT ( .MILLI., .METRE. ) );
#19425=EDGE_CURVE ( 'NONE', #16895, #6137, #15602, .T. ) ;
#19426=SURFACE_STYLE_FILL_AREA ( #13181 ) ;
#19439=ORIENTED_EDGE ( 'NONE', *, *, #1395, .T. ) ;
#19450=( LENGTH_UNIT ( ) NAMED_UNIT ( * ) SI_UNIT ( .MILLI., .METRE. ) );
#19463=COLOUR_RGB ( '', 0.31764706, 0.68627451, 0.89019608) ;
#19465=ORIENTED_EDGE ( 'NONE', *, *, #11142, .F. ) ;
#19469=STYLED_ITEM ( 'NONE', ( #7402 ), #13518 ) ;
#19519=VERTEX_POINT ( 'NONE', #17828 ) ;
#19527=DIRECTION ( 'NONE',  ( 0.000000000000000000, 1.000000000000000000, 0.000000000000000000 ) ) ;
#19529=( LENGTH_UNIT ( ) NAMED_UNIT ( * ) SI_UNIT ( .MILLI., .METRE. ) );
#19535=LINE ( 'NONE', #6999, #1926 ) ;
#19566=FACE_OUTER_BOUND ( 'NONE', #4939, .T. ) ;
#19581=UNCERTAINTY_MEASURE_WITH_UNIT (LENGTH_MEASURE( 1.000000000000000082E-05 ), #4229, 'distance_accuracy_value', 'NONE');
#19611=CARTESIAN_POINT ( 'NONE',  ( 53.48937290013659407, 127.7247684487574588, 254.0000000000000000 ) ) ;
#19628=SURFACE_STYLE_USAGE ( .BOTH. , #14715 ) ;
#19631=PLANE ( 'NONE',  #17917 ) ;
#19640=EDGE_CURVE ( 'NONE', #11794, #4707, #14956, .T. ) ;
#19645=DIRECTION ( 'NONE',  ( 0.000000000000000000, -2.352167425053297897E-16, -1.000000000000000000 ) ) ;
#19650=LINE ( 'NONE', #2839, #13358 ) ;
#19670=ADVANCED_FACE ( 'NONE', ( #15619 ), #3327, .T. ) ;
#19717=FILL_AREA_STYLE ('',( #3000 ) ) ;
#19721=MECHANICAL_DESIGN_GEOMETRIC_PRESENTATION_REPRESENTATION('',(#20044),#6928);
#19731=CARTESIAN_POINT ( 'NONE',  ( 111.4893729001366012, 129.7247684487574588, 370.0000000000000000 ) ) ;
#19737=CIRCLE ( 'NONE', #9219, 3.283624802691453848 ) ;
#19753=CARTESIAN_POINT ( 'NONE',  ( 109.4893729001365870, 211.0574367717017594, 346.4752554294135507 ) ) ;
#19785=DIRECTION ( 'NONE',  ( -9.815121534730717399E-17, 1.000000000000000000, 0.000000000000000000 ) ) ;
#19794=DIRECTION ( 'NONE',  ( 1.000000000000000000, 9.815121534730717399E-17, -0.000000000000000000 ) ) ;
#19796=ORIENTED_EDGE ( 'NONE', *, *, #8834, .F. ) ;
#19804=STYLED_ITEM ( 'NONE', ( #988 ), #12075 ) ;
#19857=CARTESIAN_POINT ( 'NONE',  ( 53.48937290013659407, 209.4935875941501422, 345.2279431939882670 ) ) ;
#19861=SURFACE_SIDE_STYLE ('',( #1835 ) ) ;
#19862=FILL_AREA_STYLE_COLOUR ( '', #5677 ) ;
#19884=DIRECTION ( 'NONE',  ( 0.000000000000000000, 0.000000000000000000, -1.000000000000000000 ) ) ;
#19885=EDGE_CURVE ( 'NONE', #8344, #4484, #13232, .T. ) ;
#19889=MECHANICAL_DESIGN_GEOMETRIC_PRESENTATION_REPRESENTATION('',(#4124),#14321);
#19891=CARTESIAN_POINT ( 'NONE',  ( 109.4893729001365870, 222.0013992467745823, 330.1364716053970483 ) ) ;
#19898=MECHANICAL_DESIGN_GEOMETRIC_PRESENTATION_REPRESENTATION('',(#10054),#2781);
#19938=CARTESIAN_POINT ( 'NONE',  ( 111.4893729001366012, 127.7247684487574304, 250.0000000000000000 ) ) ;
#19943=EDGE_CURVE ( 'NONE', #2567, #2417, #18255, .T. ) ;
#19972=EDGE_LOOP ( 'NONE', ( #3085, #12952 ) ) ;
#20018=CARTESIAN_POINT ( 'NONE',  ( 53.48937290013660828, 125.7247684487574304, 254.0000000000000000 ) ) ;
#20044=STYLED_ITEM ( 'NONE', ( #15214 ), #6916 ) ;
#20077=ORIENTED_EDGE ( 'NONE', *, *, #3986, .F. ) ;
#20093=EDGE_CURVE ( 'NONE', #19149, #17151, #10972, .T. ) ;
#20134=CYLINDRICAL_SURFACE ( 'NONE', #2647, 2.000000000000001776 ) ;
#20139=( NAMED_UNIT ( * ) SI_UNIT ( $, .STERADIAN. ) SOLID_ANGLE_UNIT ( ) );
#20147=DIRECTION ( 'NONE',  ( 0.000000000000000000, 1.000000000000000000, 0.000000000000000000 ) ) ;
#20151=DIRECTION ( 'NONE',  ( 1.000000000000000000, 9.815121534730718631E-17, -0.000000000000000000 ) ) ;
#20161=FILL_AREA_STYLE_COLOUR ( '', #1417 ) ;
#20168=CARTESIAN_POINT ( 'NONE',  ( 111.4893729001366012, 127.7247684487574588, 254.0000000000000000 ) ) ;
#20211=AXIS2_PLACEMENT_3D ( 'NONE', #14094, #3376, #19128 ) ;
#20239=CARTESIAN_POINT ( 'NONE',  ( 55.48937290013660117, 127.7247684487574588, 368.0000000000000000 ) ) ;
#20266=ORIENTED_EDGE ( 'NONE', *, *, #12519, .T. ) ;
#20272=PRESENTATION_STYLE_ASSIGNMENT (( #3058 ) ) ;
#20274=DIRECTION ( 'NONE',  ( -1.000000000000000000, -9.815121534730717399E-17, 0.000000000000000000 ) ) ;
#20281=CARTESIAN_POINT ( 'NONE',  ( 55.48937290013659407, 209.7811923590224978, 348.0151256184570343 ) ) ;
#20285=ORIENTED_EDGE ( 'NONE', *, *, #6628, .F. ) ;
#20291=ORIENTED_EDGE ( 'NONE', *, *, #16462, .T. ) ;
#20312=DIRECTION ( 'NONE',  ( 1.000000000000000000, 9.815121534730717399E-17, -0.000000000000000000 ) ) ;
#20313=EDGE_LOOP ( 'NONE', ( #7073, #11991, #16594, #11453 ) ) ;
#20321=FACE_BOUND ( 'NONE', #11384, .T. ) ;
#20346=ORIENTED_EDGE ( 'NONE', *, *, #1476, .F. ) ;
#20354=PRESENTATION_STYLE_ASSIGNMENT (( #6366 ) ) ;
#20358=ORIENTED_EDGE ( 'NONE', *, *, #20093, .F. ) ;
#20365=DIRECTION ( 'NONE',  ( 1.000000000000000000, 9.815121534730718631E-17, -0.000000000000000000 ) ) ;
ENDSEC;
END-ISO-10303-21;
